ISO-10303-21;
HEADER;
/* Generated by software containing ST-Developer
 * from STEP Tools, Inc. (www.steptools.com) 
 */

FILE_DESCRIPTION(
/* description */ (''),
/* implementation_level */ '2;1');

FILE_NAME(
/* name */ 'End_Cap.step',
/* time_stamp */ '2026-10-23T17:22:31+06:00',
/* author */ (''),
/* organization */ (''),
/* preprocessor_version */ 'ST-DEVELOPER v20.2',
/* originating_system */ 'Autodesk Translation Framework v15.15.0.0',
/* authorisation */ '');

FILE_SCHEMA (('AUTOMOTIVE_DESIGN { 1 0 10303 214 3 1 1 }'));
ENDSEC;

DATA;
#10=MECHANICAL_DESIGN_GEOMETRIC_PRESENTATION_REPRESENTATION('',(#77),#7315);
#57=SHAPE_REPRESENTATION_RELATIONSHIP('SRR','None',#7353,#67);
#67=ADVANCED_BREP_SHAPE_REPRESENTATION('',(#87),#7305);
#77=STYLED_ITEM('',(#7459),#87);
#87=MANIFOLD_SOLID_BREP('End_Cap',#3214);
#97=CONICAL_SURFACE('',#3369,10.7746348408465,0.785398163397451);
#98=CONICAL_SURFACE('',#3445,10.765215394118,0.792062411554777);
#105=B_SPLINE_CURVE_WITH_KNOTS('',3,(#4680,#4681,#4682,#4683,#4684,#4685,
#4686,#4687,#4688,#4689,#4690,#4691,#4692,#4693),.UNSPECIFIED.,.F.,.F.,
(4,2,2,2,2,2,4),(0.0797634135970256,0.102765114722899,0.137781856198111,
0.172798597673324,0.207815339148536,0.242832080623748,0.265833781749622),
 .UNSPECIFIED.);
#106=B_SPLINE_CURVE_WITH_KNOTS('',3,(#4697,#4698,#4699,#4700,#4701,#4702,
#4703,#4704,#4705,#4706,#4707,#4708,#4709,#4710),.UNSPECIFIED.,.F.,.F.,
(4,2,2,2,2,2,4),(0.466800477660132,0.490054785503752,0.525068426419775,
0.560082067335798,0.595095708251821,0.630109349167844,0.653363657011464),
 .UNSPECIFIED.);
#107=B_SPLINE_CURVE_WITH_KNOTS('',3,(#4715,#4716,#4717,#4718,#4719,#4720,
#4721,#4722,#4723,#4724,#4725,#4726,#4727,#4728),.UNSPECIFIED.,.F.,.F.,
(4,2,2,2,2,2,4),(0.0797634135970254,0.102765114722899,0.137781856198111,
0.172798597673323,0.207815339148535,0.242832080623747,0.265833781749621),
 .UNSPECIFIED.);
#108=B_SPLINE_CURVE_WITH_KNOTS('',3,(#4732,#4733,#4734,#4735,#4736,#4737,
#4738,#4739,#4740,#4741,#4742,#4743,#4744,#4745),.UNSPECIFIED.,.F.,.F.,
(4,2,2,2,2,2,4),(0.466800477660133,0.490054785503752,0.525068426419776,
0.560082067335799,0.595095708251822,0.630109349167845,0.653363657011464),
 .UNSPECIFIED.);
#109=B_SPLINE_CURVE_WITH_KNOTS('',3,(#4750,#4751,#4752,#4753,#4754,#4755,
#4756,#4757,#4758,#4759,#4760,#4761,#4762,#4763),.UNSPECIFIED.,.F.,.F.,
(4,2,2,2,2,2,4),(0.0797634135970257,0.102765114722899,0.137781856198111,
0.172798597673324,0.207815339148536,0.242832080623748,0.265833781749623),
 .UNSPECIFIED.);
#110=B_SPLINE_CURVE_WITH_KNOTS('',3,(#4767,#4768,#4769,#4770,#4771,#4772,
#4773,#4774,#4775,#4776,#4777,#4778,#4779,#4780),.UNSPECIFIED.,.F.,.F.,
(4,2,2,2,2,2,4),(0.466800477660132,0.490054785503751,0.525068426419774,
0.560082067335798,0.595095708251821,0.630109349167844,0.653363657011463),
 .UNSPECIFIED.);
#111=B_SPLINE_CURVE_WITH_KNOTS('',3,(#4785,#4786,#4787,#4788,#4789,#4790,
#4791,#4792,#4793,#4794,#4795,#4796,#4797,#4798),.UNSPECIFIED.,.F.,.F.,
(4,2,2,2,2,2,4),(0.0797634135970255,0.102765114722899,0.137781856198111,
0.172798597673323,0.207815339148536,0.242832080623748,0.265833781749622),
 .UNSPECIFIED.);
#112=B_SPLINE_CURVE_WITH_KNOTS('',3,(#4802,#4803,#4804,#4805,#4806,#4807,
#4808,#4809,#4810,#4811,#4812,#4813,#4814,#4815),.UNSPECIFIED.,.F.,.F.,
(4,2,2,2,2,2,4),(0.466800477660132,0.490054785503752,0.525068426419775,
0.560082067335798,0.595095708251821,0.630109349167844,0.653363657011464),
 .UNSPECIFIED.);
#113=B_SPLINE_CURVE_WITH_KNOTS('',3,(#4820,#4821,#4822,#4823,#4824,#4825,
#4826,#4827,#4828,#4829,#4830,#4831,#4832,#4833),.UNSPECIFIED.,.F.,.F.,
(4,2,2,2,2,2,4),(0.0797634135970245,0.102765114722899,0.137781856198111,
0.172798597673324,0.207815339148536,0.242832080623748,0.265833781749621),
 .UNSPECIFIED.);
#114=B_SPLINE_CURVE_WITH_KNOTS('',3,(#4837,#4838,#4839,#4840,#4841,#4842,
#4843,#4844,#4845,#4846,#4847,#4848,#4849,#4850),.UNSPECIFIED.,.F.,.F.,
(4,2,2,2,2,2,4),(0.466800477660132,0.490054785503751,0.525068426419774,
0.560082067335797,0.59509570825182,0.630109349167844,0.653363657011463),
 .UNSPECIFIED.);
#115=B_SPLINE_CURVE_WITH_KNOTS('',3,(#4855,#4856,#4857,#4858,#4859,#4860,
#4861,#4862,#4863,#4864,#4865,#4866,#4867,#4868),.UNSPECIFIED.,.F.,.F.,
(4,2,2,2,2,2,4),(0.0797634135970255,0.102765114722899,0.137781856198111,
0.172798597673324,0.207815339148536,0.242832080623748,0.265833781749622),
 .UNSPECIFIED.);
#116=B_SPLINE_CURVE_WITH_KNOTS('',3,(#4872,#4873,#4874,#4875,#4876,#4877,
#4878,#4879,#4880,#4881,#4882,#4883,#4884,#4885),.UNSPECIFIED.,.F.,.F.,
(4,2,2,2,2,2,4),(0.466800477660132,0.490054785503752,0.525068426419775,
0.560082067335798,0.595095708251821,0.630109349167844,0.653363657011464),
 .UNSPECIFIED.);
#117=B_SPLINE_CURVE_WITH_KNOTS('',3,(#4890,#4891,#4892,#4893,#4894,#4895,
#4896,#4897,#4898,#4899,#4900,#4901,#4902,#4903),.UNSPECIFIED.,.F.,.F.,
(4,2,2,2,2,2,4),(0.0797634135970254,0.102765114722899,0.137781856198111,
0.172798597673323,0.207815339148536,0.242832080623748,0.265833781749621),
 .UNSPECIFIED.);
#118=B_SPLINE_CURVE_WITH_KNOTS('',3,(#4907,#4908,#4909,#4910,#4911,#4912,
#4913,#4914,#4915,#4916,#4917,#4918,#4919,#4920),.UNSPECIFIED.,.F.,.F.,
(4,2,2,2,2,2,4),(0.466800477660132,0.490054785503752,0.525068426419775,
0.560082067335798,0.595095708251821,0.630109349167844,0.653363657011464),
 .UNSPECIFIED.);
#119=B_SPLINE_CURVE_WITH_KNOTS('',3,(#4925,#4926,#4927,#4928,#4929,#4930,
#4931,#4932,#4933,#4934,#4935,#4936,#4937,#4938),.UNSPECIFIED.,.F.,.F.,
(4,2,2,2,2,2,4),(0.0797634135970265,0.1027651147229,0.137781856198112,0.172798597673324,
0.207815339148536,0.242832080623748,0.265833781749622),.UNSPECIFIED.);
#120=B_SPLINE_CURVE_WITH_KNOTS('',3,(#4942,#4943,#4944,#4945,#4946,#4947,
#4948,#4949,#4950,#4951,#4952,#4953,#4954,#4955),.UNSPECIFIED.,.F.,.F.,
(4,2,2,2,2,2,4),(0.466800477660132,0.490054785503752,0.525068426419775,
0.560082067335798,0.595095708251821,0.630109349167844,0.653363657011464),
 .UNSPECIFIED.);
#121=B_SPLINE_CURVE_WITH_KNOTS('',3,(#4960,#4961,#4962,#4963,#4964,#4965,
#4966,#4967,#4968,#4969,#4970,#4971,#4972,#4973),.UNSPECIFIED.,.F.,.F.,
(4,2,2,2,2,2,4),(0.0797634135970254,0.102765114722899,0.137781856198111,
0.172798597673323,0.207815339148535,0.242832080623747,0.265833781749621),
 .UNSPECIFIED.);
#122=B_SPLINE_CURVE_WITH_KNOTS('',3,(#4977,#4978,#4979,#4980,#4981,#4982,
#4983,#4984,#4985,#4986,#4987,#4988,#4989,#4990),.UNSPECIFIED.,.F.,.F.,
(4,2,2,2,2,2,4),(0.466800477660131,0.490054785503751,0.525068426419774,
0.560082067335798,0.59509570825182,0.630109349167843,0.653363657011463),
 .UNSPECIFIED.);
#123=B_SPLINE_CURVE_WITH_KNOTS('',3,(#4995,#4996,#4997,#4998,#4999,#5000,
#5001,#5002,#5003,#5004,#5005,#5006,#5007,#5008),.UNSPECIFIED.,.F.,.F.,
(4,2,2,2,2,2,4),(0.0797634135970272,0.102765114722899,0.137781856198112,
0.172798597673324,0.207815339148536,0.242832080623748,0.265833781749622),
 .UNSPECIFIED.);
#124=B_SPLINE_CURVE_WITH_KNOTS('',3,(#5012,#5013,#5014,#5015,#5016,#5017,
#5018,#5019,#5020,#5021,#5022,#5023,#5024,#5025),.UNSPECIFIED.,.F.,.F.,
(4,2,2,2,2,2,4),(0.466800477660132,0.490054785503752,0.525068426419775,
0.560082067335798,0.595095708251821,0.630109349167844,0.653363657011464),
 .UNSPECIFIED.);
#125=B_SPLINE_CURVE_WITH_KNOTS('',3,(#5030,#5031,#5032,#5033,#5034,#5035,
#5036,#5037,#5038,#5039,#5040,#5041,#5042,#5043),.UNSPECIFIED.,.F.,.F.,
(4,2,2,2,2,2,4),(0.0797634135970255,0.102765114722899,0.137781856198111,
0.172798597673323,0.207815339148535,0.242832080623748,0.265833781749622),
 .UNSPECIFIED.);
#126=B_SPLINE_CURVE_WITH_KNOTS('',3,(#5047,#5048,#5049,#5050,#5051,#5052,
#5053,#5054,#5055,#5056,#5057,#5058,#5059,#5060),.UNSPECIFIED.,.F.,.F.,
(4,2,2,2,2,2,4),(0.466800477660132,0.490054785503752,0.525068426419775,
0.560082067335798,0.595095708251821,0.630109349167844,0.653363657011464),
 .UNSPECIFIED.);
#127=B_SPLINE_CURVE_WITH_KNOTS('',3,(#5065,#5066,#5067,#5068,#5069,#5070,
#5071,#5072,#5073,#5074,#5075,#5076,#5077,#5078),.UNSPECIFIED.,.F.,.F.,
(4,2,2,2,2,2,4),(0.0797634135970258,0.102765114722899,0.137781856198111,
0.172798597673324,0.207815339148536,0.242832080623748,0.265833781749623),
 .UNSPECIFIED.);
#128=B_SPLINE_CURVE_WITH_KNOTS('',3,(#5082,#5083,#5084,#5085,#5086,#5087,
#5088,#5089,#5090,#5091,#5092,#5093,#5094,#5095),.UNSPECIFIED.,.F.,.F.,
(4,2,2,2,2,2,4),(0.466800477660132,0.490054785503751,0.525068426419774,
0.560082067335797,0.59509570825182,0.630109349167844,0.653363657011463),
 .UNSPECIFIED.);
#129=B_SPLINE_CURVE_WITH_KNOTS('',3,(#5100,#5101,#5102,#5103,#5104,#5105,
#5106,#5107,#5108,#5109,#5110,#5111,#5112,#5113),.UNSPECIFIED.,.F.,.F.,
(4,2,2,2,2,2,4),(0.0797634135970256,0.102765114722899,0.137781856198111,
0.172798597673324,0.207815339148536,0.242832080623748,0.265833781749621),
 .UNSPECIFIED.);
#130=B_SPLINE_CURVE_WITH_KNOTS('',3,(#5117,#5118,#5119,#5120,#5121,#5122,
#5123,#5124,#5125,#5126,#5127,#5128,#5129,#5130),.UNSPECIFIED.,.F.,.F.,
(4,2,2,2,2,2,4),(0.466800477660132,0.490054785503751,0.525068426419774,
0.560082067335797,0.595095708251821,0.630109349167844,0.653363657011463),
 .UNSPECIFIED.);
#131=B_SPLINE_CURVE_WITH_KNOTS('',3,(#5135,#5136,#5137,#5138,#5139,#5140,
#5141,#5142,#5143,#5144,#5145,#5146,#5147,#5148),.UNSPECIFIED.,.F.,.F.,
(4,2,2,2,2,2,4),(0.0797634135970255,0.102765114722899,0.137781856198111,
0.172798597673323,0.207815339148536,0.242832080623748,0.265833781749622),
 .UNSPECIFIED.);
#132=B_SPLINE_CURVE_WITH_KNOTS('',3,(#5152,#5153,#5154,#5155,#5156,#5157,
#5158,#5159,#5160,#5161,#5162,#5163,#5164,#5165),.UNSPECIFIED.,.F.,.F.,
(4,2,2,2,2,2,4),(0.466800477660132,0.490054785503751,0.525068426419775,
0.560082067335798,0.595095708251821,0.630109349167844,0.653363657011464),
 .UNSPECIFIED.);
#133=B_SPLINE_CURVE_WITH_KNOTS('',3,(#5170,#5171,#5172,#5173,#5174,#5175,
#5176,#5177,#5178,#5179,#5180,#5181,#5182,#5183),.UNSPECIFIED.,.F.,.F.,
(4,2,2,2,2,2,4),(0.0797634135970253,0.102765114722899,0.137781856198111,
0.172798597673323,0.207815339148536,0.242832080623748,0.265833781749621),
 .UNSPECIFIED.);
#134=B_SPLINE_CURVE_WITH_KNOTS('',3,(#5187,#5188,#5189,#5190,#5191,#5192,
#5193,#5194,#5195,#5196,#5197,#5198,#5199,#5200),.UNSPECIFIED.,.F.,.F.,
(4,2,2,2,2,2,4),(0.466800477660132,0.490054785503751,0.525068426419775,
0.560082067335798,0.595095708251821,0.630109349167844,0.653363657011464),
 .UNSPECIFIED.);
#135=B_SPLINE_CURVE_WITH_KNOTS('',3,(#5205,#5206,#5207,#5208,#5209,#5210,
#5211,#5212,#5213,#5214,#5215,#5216,#5217,#5218),.UNSPECIFIED.,.F.,.F.,
(4,2,2,2,2,2,4),(0.0797634135970255,0.102765114722899,0.137781856198111,
0.172798597673323,0.207815339148536,0.242832080623748,0.265833781749622),
 .UNSPECIFIED.);
#136=B_SPLINE_CURVE_WITH_KNOTS('',3,(#5222,#5223,#5224,#5225,#5226,#5227,
#5228,#5229,#5230,#5231,#5232,#5233,#5234,#5235),.UNSPECIFIED.,.F.,.F.,
(4,2,2,2,2,2,4),(0.466800477660132,0.490054785503751,0.525068426419775,
0.560082067335798,0.595095708251821,0.630109349167844,0.653363657011463),
 .UNSPECIFIED.);
#137=B_SPLINE_CURVE_WITH_KNOTS('',3,(#5240,#5241,#5242,#5243,#5244,#5245,
#5246,#5247,#5248,#5249,#5250,#5251,#5252,#5253),.UNSPECIFIED.,.F.,.F.,
(4,2,2,2,2,2,4),(0.0797634135970254,0.102765114722899,0.137781856198111,
0.172798597673323,0.207815339148535,0.242832080623747,0.265833781749621),
 .UNSPECIFIED.);
#138=B_SPLINE_CURVE_WITH_KNOTS('',3,(#5257,#5258,#5259,#5260,#5261,#5262,
#5263,#5264,#5265,#5266,#5267,#5268,#5269,#5270),.UNSPECIFIED.,.F.,.F.,
(4,2,2,2,2,2,4),(0.466800477660132,0.490054785503752,0.525068426419775,
0.560082067335798,0.595095708251821,0.630109349167844,0.653363657011464),
 .UNSPECIFIED.);
#139=B_SPLINE_CURVE_WITH_KNOTS('',3,(#5275,#5276,#5277,#5278,#5279,#5280,
#5281,#5282,#5283,#5284,#5285,#5286,#5287,#5288),.UNSPECIFIED.,.F.,.F.,
(4,2,2,2,2,2,4),(0.0797634135970276,0.102765114722899,0.137781856198111,
0.172798597673324,0.207815339148536,0.242832080623748,0.265833781749621),
 .UNSPECIFIED.);
#140=B_SPLINE_CURVE_WITH_KNOTS('',3,(#5292,#5293,#5294,#5295,#5296,#5297,
#5298,#5299,#5300,#5301,#5302,#5303,#5304,#5305),.UNSPECIFIED.,.F.,.F.,
(4,2,2,2,2,2,4),(0.466800477660133,0.490054785503752,0.525068426419776,
0.560082067335799,0.595095708251822,0.630109349167845,0.653363657011464),
 .UNSPECIFIED.);
#141=B_SPLINE_CURVE_WITH_KNOTS('',3,(#5310,#5311,#5312,#5313,#5314,#5315,
#5316,#5317,#5318,#5319,#5320,#5321,#5322,#5323),.UNSPECIFIED.,.F.,.F.,
(4,2,2,2,2,2,4),(0.0797634135970256,0.102765114722899,0.137781856198112,
0.172798597673324,0.207815339148536,0.242832080623748,0.265833781749622),
 .UNSPECIFIED.);
#142=B_SPLINE_CURVE_WITH_KNOTS('',3,(#5327,#5328,#5329,#5330,#5331,#5332,
#5333,#5334,#5335,#5336,#5337,#5338,#5339,#5340),.UNSPECIFIED.,.F.,.F.,
(4,2,2,2,2,2,4),(0.466800477660132,0.490054785503752,0.525068426419775,
0.560082067335798,0.595095708251822,0.630109349167845,0.653363657011465),
 .UNSPECIFIED.);
#143=B_SPLINE_CURVE_WITH_KNOTS('',3,(#5345,#5346,#5347,#5348,#5349,#5350,
#5351,#5352,#5353,#5354,#5355,#5356,#5357,#5358),.UNSPECIFIED.,.F.,.F.,
(4,2,2,2,2,2,4),(0.0797634135970255,0.102765114722899,0.137781856198111,
0.172798597673323,0.207815339148536,0.242832080623748,0.265833781749621),
 .UNSPECIFIED.);
#144=B_SPLINE_CURVE_WITH_KNOTS('',3,(#5362,#5363,#5364,#5365,#5366,#5367,
#5368,#5369,#5370,#5371,#5372,#5373,#5374,#5375),.UNSPECIFIED.,.F.,.F.,
(4,2,2,2,2,2,4),(0.466800477660133,0.490054785503752,0.525068426419775,
0.560082067335798,0.595095708251821,0.630109349167844,0.653363657011464),
 .UNSPECIFIED.);
#145=B_SPLINE_CURVE_WITH_KNOTS('',3,(#5380,#5381,#5382,#5383,#5384,#5385,
#5386,#5387,#5388,#5389,#5390,#5391,#5392,#5393),.UNSPECIFIED.,.F.,.F.,
(4,2,2,2,2,2,4),(0.0797634135970255,0.102765114722899,0.137781856198111,
0.172798597673323,0.207815339148536,0.242832080623748,0.265833781749621),
 .UNSPECIFIED.);
#146=B_SPLINE_CURVE_WITH_KNOTS('',3,(#5397,#5398,#5399,#5400,#5401,#5402,
#5403,#5404,#5405,#5406,#5407,#5408,#5409,#5410),.UNSPECIFIED.,.F.,.F.,
(4,2,2,2,2,2,4),(0.466800477660132,0.490054785503752,0.525068426419775,
0.560082067335798,0.595095708251821,0.630109349167844,0.653363657011464),
 .UNSPECIFIED.);
#147=B_SPLINE_CURVE_WITH_KNOTS('',3,(#5415,#5416,#5417,#5418,#5419,#5420,
#5421,#5422,#5423,#5424,#5425,#5426,#5427,#5428),.UNSPECIFIED.,.F.,.F.,
(4,2,2,2,2,2,4),(0.0797634135970255,0.102765114722899,0.137781856198111,
0.172798597673324,0.207815339148536,0.242832080623748,0.265833781749623),
 .UNSPECIFIED.);
#148=B_SPLINE_CURVE_WITH_KNOTS('',3,(#5432,#5433,#5434,#5435,#5436,#5437,
#5438,#5439,#5440,#5441,#5442,#5443,#5444,#5445),.UNSPECIFIED.,.F.,.F.,
(4,2,2,2,2,2,4),(0.466800477660132,0.490054785503752,0.525068426419775,
0.560082067335798,0.595095708251821,0.630109349167844,0.653363657011463),
 .UNSPECIFIED.);
#149=B_SPLINE_CURVE_WITH_KNOTS('',3,(#5450,#5451,#5452,#5453,#5454,#5455,
#5456,#5457,#5458,#5459,#5460,#5461,#5462,#5463),.UNSPECIFIED.,.F.,.F.,
(4,2,2,2,2,2,4),(0.0797634135970256,0.102765114722899,0.137781856198111,
0.172798597673323,0.207815339148536,0.242832080623748,0.265833781749621),
 .UNSPECIFIED.);
#150=B_SPLINE_CURVE_WITH_KNOTS('',3,(#5467,#5468,#5469,#5470,#5471,#5472,
#5473,#5474,#5475,#5476,#5477,#5478,#5479,#5480),.UNSPECIFIED.,.F.,.F.,
(4,2,2,2,2,2,4),(0.466800477660132,0.490054785503752,0.525068426419775,
0.560082067335798,0.595095708251821,0.630109349167844,0.653363657011463),
 .UNSPECIFIED.);
#151=B_SPLINE_CURVE_WITH_KNOTS('',3,(#5485,#5486,#5487,#5488,#5489,#5490,
#5491,#5492,#5493,#5494,#5495,#5496,#5497,#5498),.UNSPECIFIED.,.F.,.F.,
(4,2,2,2,2,2,4),(0.0797634135970257,0.102765114722899,0.137781856198111,
0.172798597673324,0.207815339148536,0.242832080623748,0.265833781749622),
 .UNSPECIFIED.);
#152=B_SPLINE_CURVE_WITH_KNOTS('',3,(#5502,#5503,#5504,#5505,#5506,#5507,
#5508,#5509,#5510,#5511,#5512,#5513,#5514,#5515),.UNSPECIFIED.,.F.,.F.,
(4,2,2,2,2,2,4),(0.466800477660132,0.490054785503752,0.525068426419775,
0.560082067335798,0.595095708251821,0.630109349167844,0.653363657011463),
 .UNSPECIFIED.);
#153=B_SPLINE_CURVE_WITH_KNOTS('',3,(#5523,#5524,#5525,#5526,#5527,#5528,
#5529,#5530),.UNSPECIFIED.,.F.,.F.,(4,2,2,4),(0.560082067335798,0.595095708251821,
0.630109349167844,0.653363657011463),.UNSPECIFIED.);
#154=B_SPLINE_CURVE_WITH_KNOTS('',3,(#5557,#5558,#5559,#5560,#5561,#5562,
#5563,#5564),.UNSPECIFIED.,.F.,.F.,(4,2,2,4),(0.466800477660132,0.490054785503752,
0.525068426419775,0.560082067335798),.UNSPECIFIED.);
#155=B_SPLINE_CURVE_WITH_KNOTS('',3,(#5619,#5620,#5621,#5622,#5623,#5624,
#5625,#5626),.UNSPECIFIED.,.F.,.F.,(4,2,2,4),(0.0797634135970255,0.102765114722899,
0.137781856198111,0.172798597673323),.UNSPECIFIED.);
#156=B_SPLINE_CURVE_WITH_KNOTS('',3,(#5627,#5628,#5629,#5630,#5631,#5632,
#5633,#5634),.UNSPECIFIED.,.F.,.F.,(4,2,2,4),(0.172798597673323,0.207815339148535,
0.242832080623748,0.265833781749621),.UNSPECIFIED.);
#229=LINE('',#4676,#389);
#230=LINE('',#4695,#390);
#231=LINE('',#4711,#391);
#232=LINE('',#4730,#392);
#233=LINE('',#4746,#393);
#234=LINE('',#4765,#394);
#235=LINE('',#4781,#395);
#236=LINE('',#4800,#396);
#237=LINE('',#4816,#397);
#238=LINE('',#4835,#398);
#239=LINE('',#4851,#399);
#240=LINE('',#4870,#400);
#241=LINE('',#4886,#401);
#242=LINE('',#4905,#402);
#243=LINE('',#4921,#403);
#244=LINE('',#4940,#404);
#245=LINE('',#4956,#405);
#246=LINE('',#4975,#406);
#247=LINE('',#4991,#407);
#248=LINE('',#5010,#408);
#249=LINE('',#5026,#409);
#250=LINE('',#5045,#410);
#251=LINE('',#5061,#411);
#252=LINE('',#5080,#412);
#253=LINE('',#5096,#413);
#254=LINE('',#5115,#414);
#255=LINE('',#5131,#415);
#256=LINE('',#5150,#416);
#257=LINE('',#5166,#417);
#258=LINE('',#5185,#418);
#259=LINE('',#5201,#419);
#260=LINE('',#5220,#420);
#261=LINE('',#5236,#421);
#262=LINE('',#5255,#422);
#263=LINE('',#5271,#423);
#264=LINE('',#5290,#424);
#265=LINE('',#5306,#425);
#266=LINE('',#5325,#426);
#267=LINE('',#5341,#427);
#268=LINE('',#5360,#428);
#269=LINE('',#5376,#429);
#270=LINE('',#5395,#430);
#271=LINE('',#5411,#431);
#272=LINE('',#5430,#432);
#273=LINE('',#5446,#433);
#274=LINE('',#5465,#434);
#275=LINE('',#5481,#435);
#276=LINE('',#5500,#436);
#277=LINE('',#5516,#437);
#278=LINE('',#5521,#438);
#279=LINE('',#5568,#439);
#280=LINE('',#5571,#440);
#281=LINE('',#5637,#441);
#282=LINE('',#5644,#442);
#389=VECTOR('',#3744,10.5057959473896);
#390=VECTOR('',#3747,10.);
#391=VECTOR('',#3748,10.);
#392=VECTOR('',#3751,10.);
#393=VECTOR('',#3752,10.);
#394=VECTOR('',#3755,10.);
#395=VECTOR('',#3756,10.);
#396=VECTOR('',#3759,10.);
#397=VECTOR('',#3760,10.);
#398=VECTOR('',#3763,10.);
#399=VECTOR('',#3764,10.);
#400=VECTOR('',#3767,10.);
#401=VECTOR('',#3768,10.);
#402=VECTOR('',#3771,10.);
#403=VECTOR('',#3772,10.);
#404=VECTOR('',#3775,10.);
#405=VECTOR('',#3776,10.);
#406=VECTOR('',#3779,10.);
#407=VECTOR('',#3780,10.);
#408=VECTOR('',#3783,10.);
#409=VECTOR('',#3784,10.);
#410=VECTOR('',#3787,10.);
#411=VECTOR('',#3788,10.);
#412=VECTOR('',#3791,10.);
#413=VECTOR('',#3792,10.);
#414=VECTOR('',#3795,10.);
#415=VECTOR('',#3796,10.);
#416=VECTOR('',#3799,10.);
#417=VECTOR('',#3800,10.);
#418=VECTOR('',#3803,10.);
#419=VECTOR('',#3804,10.);
#420=VECTOR('',#3807,10.);
#421=VECTOR('',#3808,10.);
#422=VECTOR('',#3811,10.);
#423=VECTOR('',#3812,10.);
#424=VECTOR('',#3815,10.);
#425=VECTOR('',#3816,10.);
#426=VECTOR('',#3819,10.);
#427=VECTOR('',#3820,10.);
#428=VECTOR('',#3823,10.);
#429=VECTOR('',#3824,10.);
#430=VECTOR('',#3827,10.);
#431=VECTOR('',#3828,10.);
#432=VECTOR('',#3831,10.);
#433=VECTOR('',#3832,10.);
#434=VECTOR('',#3835,10.);
#435=VECTOR('',#3836,10.);
#436=VECTOR('',#3839,10.);
#437=VECTOR('',#3840,10.);
#438=VECTOR('',#3845,10.7746348408465);
#439=VECTOR('',#3900,10.);
#440=VECTOR('',#3903,10.);
#441=VECTOR('',#4000,10.765215394118);
#442=VECTOR('',#4011,9.50579594738959);
#549=CYLINDRICAL_SURFACE('',#3343,10.5057959473896);
#550=CYLINDRICAL_SURFACE('',#3345,0.999999999999999);
#551=CYLINDRICAL_SURFACE('',#3346,0.999999999999999);
#552=CYLINDRICAL_SURFACE('',#3347,0.999999999999999);
#553=CYLINDRICAL_SURFACE('',#3348,0.999999999999999);
#554=CYLINDRICAL_SURFACE('',#3349,0.999999999999999);
#555=CYLINDRICAL_SURFACE('',#3350,0.999999999999999);
#556=CYLINDRICAL_SURFACE('',#3351,0.999999999999999);
#557=CYLINDRICAL_SURFACE('',#3352,0.999999999999999);
#558=CYLINDRICAL_SURFACE('',#3353,0.999999999999999);
#559=CYLINDRICAL_SURFACE('',#3354,0.999999999999999);
#560=CYLINDRICAL_SURFACE('',#3355,0.999999999999999);
#561=CYLINDRICAL_SURFACE('',#3356,0.999999999999999);
#562=CYLINDRICAL_SURFACE('',#3357,0.999999999999999);
#563=CYLINDRICAL_SURFACE('',#3358,0.999999999999999);
#564=CYLINDRICAL_SURFACE('',#3359,0.999999999999999);
#565=CYLINDRICAL_SURFACE('',#3360,0.999999999999999);
#566=CYLINDRICAL_SURFACE('',#3361,0.999999999999999);
#567=CYLINDRICAL_SURFACE('',#3362,0.999999999999999);
#568=CYLINDRICAL_SURFACE('',#3363,0.999999999999999);
#569=CYLINDRICAL_SURFACE('',#3364,0.999999999999999);
#570=CYLINDRICAL_SURFACE('',#3365,0.999999999999999);
#571=CYLINDRICAL_SURFACE('',#3366,0.999999999999999);
#572=CYLINDRICAL_SURFACE('',#3367,0.999999999999999);
#573=CYLINDRICAL_SURFACE('',#3368,0.999999999999999);
#574=CYLINDRICAL_SURFACE('',#3396,11.0246348408465);
#575=CYLINDRICAL_SURFACE('',#3398,11.0246348408465);
#576=CYLINDRICAL_SURFACE('',#3400,11.0246348408465);
#577=CYLINDRICAL_SURFACE('',#3402,11.0246348408465);
#578=CYLINDRICAL_SURFACE('',#3404,11.0246348408465);
#579=CYLINDRICAL_SURFACE('',#3406,11.0246348408465);
#580=CYLINDRICAL_SURFACE('',#3408,11.0246348408465);
#581=CYLINDRICAL_SURFACE('',#3410,11.0246348408465);
#582=CYLINDRICAL_SURFACE('',#3412,11.0246348408465);
#583=CYLINDRICAL_SURFACE('',#3414,11.0246348408465);
#584=CYLINDRICAL_SURFACE('',#3416,11.0246348408465);
#585=CYLINDRICAL_SURFACE('',#3418,11.0246348408465);
#586=CYLINDRICAL_SURFACE('',#3420,11.0246348408465);
#587=CYLINDRICAL_SURFACE('',#3422,11.0246348408465);
#588=CYLINDRICAL_SURFACE('',#3424,11.0246348408465);
#589=CYLINDRICAL_SURFACE('',#3426,11.0246348408465);
#590=CYLINDRICAL_SURFACE('',#3428,11.0246348408465);
#591=CYLINDRICAL_SURFACE('',#3430,11.0246348408465);
#592=CYLINDRICAL_SURFACE('',#3432,11.0246348408465);
#593=CYLINDRICAL_SURFACE('',#3434,11.0246348408465);
#594=CYLINDRICAL_SURFACE('',#3436,11.0246348408465);
#595=CYLINDRICAL_SURFACE('',#3438,11.0246348408465);
#596=CYLINDRICAL_SURFACE('',#3440,11.0246348408465);
#597=CYLINDRICAL_SURFACE('',#3442,11.0246348408465);
#598=CYLINDRICAL_SURFACE('',#3444,0.999999999999999);
#599=CYLINDRICAL_SURFACE('',#3447,11.0246348408465);
#600=CYLINDRICAL_SURFACE('',#3451,9.50579594738959);
#689=FACE_BOUND('',#912,.T.);
#700=PLANE('',#3341);
#701=PLANE('',#3448);
#702=PLANE('',#3449);
#728=FACE_OUTER_BOUND('',#910,.T.);
#729=FACE_OUTER_BOUND('',#911,.T.);
#730=FACE_OUTER_BOUND('',#913,.T.);
#731=FACE_OUTER_BOUND('',#914,.T.);
#732=FACE_OUTER_BOUND('',#915,.T.);
#733=FACE_OUTER_BOUND('',#916,.T.);
#734=FACE_OUTER_BOUND('',#917,.T.);
#735=FACE_OUTER_BOUND('',#918,.T.);
#736=FACE_OUTER_BOUND('',#919,.T.);
#737=FACE_OUTER_BOUND('',#920,.T.);
#738=FACE_OUTER_BOUND('',#921,.T.);
#739=FACE_OUTER_BOUND('',#922,.T.);
#740=FACE_OUTER_BOUND('',#923,.T.);
#741=FACE_OUTER_BOUND('',#924,.T.);
#742=FACE_OUTER_BOUND('',#925,.T.);
#743=FACE_OUTER_BOUND('',#926,.T.);
#744=FACE_OUTER_BOUND('',#927,.T.);
#745=FACE_OUTER_BOUND('',#928,.T.);
#746=FACE_OUTER_BOUND('',#929,.T.);
#747=FACE_OUTER_BOUND('',#930,.T.);
#748=FACE_OUTER_BOUND('',#931,.T.);
#749=FACE_OUTER_BOUND('',#932,.T.);
#750=FACE_OUTER_BOUND('',#933,.T.);
#751=FACE_OUTER_BOUND('',#934,.T.);
#752=FACE_OUTER_BOUND('',#935,.T.);
#753=FACE_OUTER_BOUND('',#936,.T.);
#754=FACE_OUTER_BOUND('',#937,.T.);
#755=FACE_OUTER_BOUND('',#938,.T.);
#756=FACE_OUTER_BOUND('',#939,.T.);
#757=FACE_OUTER_BOUND('',#940,.T.);
#758=FACE_OUTER_BOUND('',#941,.T.);
#759=FACE_OUTER_BOUND('',#942,.T.);
#760=FACE_OUTER_BOUND('',#943,.T.);
#761=FACE_OUTER_BOUND('',#944,.T.);
#762=FACE_OUTER_BOUND('',#945,.T.);
#763=FACE_OUTER_BOUND('',#946,.T.);
#764=FACE_OUTER_BOUND('',#947,.T.);
#765=FACE_OUTER_BOUND('',#948,.T.);
#766=FACE_OUTER_BOUND('',#949,.T.);
#767=FACE_OUTER_BOUND('',#950,.T.);
#768=FACE_OUTER_BOUND('',#951,.T.);
#769=FACE_OUTER_BOUND('',#952,.T.);
#770=FACE_OUTER_BOUND('',#953,.T.);
#771=FACE_OUTER_BOUND('',#954,.T.);
#772=FACE_OUTER_BOUND('',#955,.T.);
#773=FACE_OUTER_BOUND('',#956,.T.);
#774=FACE_OUTER_BOUND('',#957,.T.);
#775=FACE_OUTER_BOUND('',#958,.T.);
#776=FACE_OUTER_BOUND('',#959,.T.);
#777=FACE_OUTER_BOUND('',#960,.T.);
#778=FACE_OUTER_BOUND('',#961,.T.);
#779=FACE_OUTER_BOUND('',#962,.T.);
#780=FACE_OUTER_BOUND('',#963,.T.);
#781=FACE_OUTER_BOUND('',#964,.T.);
#782=FACE_OUTER_BOUND('',#965,.T.);
#783=FACE_OUTER_BOUND('',#966,.T.);
#784=FACE_OUTER_BOUND('',#967,.T.);
#785=FACE_OUTER_BOUND('',#968,.T.);
#910=EDGE_LOOP('',(#2080,#2081,#2082,#2083));
#911=EDGE_LOOP('',(#2084));
#912=EDGE_LOOP('',(#2085));
#913=EDGE_LOOP('',(#2086,#2087,#2088,#2089));
#914=EDGE_LOOP('',(#2090,#2091,#2092,#2093));
#915=EDGE_LOOP('',(#2094,#2095,#2096,#2097));
#916=EDGE_LOOP('',(#2098,#2099,#2100,#2101));
#917=EDGE_LOOP('',(#2102,#2103,#2104,#2105));
#918=EDGE_LOOP('',(#2106,#2107,#2108,#2109));
#919=EDGE_LOOP('',(#2110,#2111,#2112,#2113));
#920=EDGE_LOOP('',(#2114,#2115,#2116,#2117));
#921=EDGE_LOOP('',(#2118,#2119,#2120,#2121));
#922=EDGE_LOOP('',(#2122,#2123,#2124,#2125));
#923=EDGE_LOOP('',(#2126,#2127,#2128,#2129));
#924=EDGE_LOOP('',(#2130,#2131,#2132,#2133));
#925=EDGE_LOOP('',(#2134,#2135,#2136,#2137));
#926=EDGE_LOOP('',(#2138,#2139,#2140,#2141));
#927=EDGE_LOOP('',(#2142,#2143,#2144,#2145));
#928=EDGE_LOOP('',(#2146,#2147,#2148,#2149));
#929=EDGE_LOOP('',(#2150,#2151,#2152,#2153));
#930=EDGE_LOOP('',(#2154,#2155,#2156,#2157));
#931=EDGE_LOOP('',(#2158,#2159,#2160,#2161));
#932=EDGE_LOOP('',(#2162,#2163,#2164,#2165));
#933=EDGE_LOOP('',(#2166,#2167,#2168,#2169));
#934=EDGE_LOOP('',(#2170,#2171,#2172,#2173));
#935=EDGE_LOOP('',(#2174,#2175,#2176,#2177));
#936=EDGE_LOOP('',(#2178,#2179,#2180,#2181));
#937=EDGE_LOOP('',(#2182,#2183,#2184,#2185));
#938=EDGE_LOOP('',(#2186,#2187,#2188,#2189,#2190,#2191,#2192,#2193,#2194,
#2195,#2196,#2197,#2198,#2199,#2200,#2201,#2202,#2203,#2204,#2205,#2206,
#2207,#2208,#2209,#2210,#2211,#2212,#2213,#2214,#2215,#2216,#2217,#2218,
#2219,#2220,#2221,#2222,#2223,#2224,#2225,#2226,#2227,#2228,#2229,#2230,
#2231,#2232,#2233,#2234,#2235,#2236,#2237,#2238,#2239));
#939=EDGE_LOOP('',(#2240,#2241,#2242,#2243));
#940=EDGE_LOOP('',(#2244,#2245,#2246,#2247));
#941=EDGE_LOOP('',(#2248,#2249,#2250,#2251));
#942=EDGE_LOOP('',(#2252,#2253,#2254,#2255));
#943=EDGE_LOOP('',(#2256,#2257,#2258,#2259));
#944=EDGE_LOOP('',(#2260,#2261,#2262,#2263));
#945=EDGE_LOOP('',(#2264,#2265,#2266,#2267));
#946=EDGE_LOOP('',(#2268,#2269,#2270,#2271));
#947=EDGE_LOOP('',(#2272,#2273,#2274,#2275));
#948=EDGE_LOOP('',(#2276,#2277,#2278,#2279));
#949=EDGE_LOOP('',(#2280,#2281,#2282,#2283));
#950=EDGE_LOOP('',(#2284,#2285,#2286,#2287));
#951=EDGE_LOOP('',(#2288,#2289,#2290,#2291));
#952=EDGE_LOOP('',(#2292,#2293,#2294,#2295));
#953=EDGE_LOOP('',(#2296,#2297,#2298,#2299));
#954=EDGE_LOOP('',(#2300,#2301,#2302,#2303));
#955=EDGE_LOOP('',(#2304,#2305,#2306,#2307));
#956=EDGE_LOOP('',(#2308,#2309,#2310,#2311));
#957=EDGE_LOOP('',(#2312,#2313,#2314,#2315));
#958=EDGE_LOOP('',(#2316,#2317,#2318,#2319));
#959=EDGE_LOOP('',(#2320,#2321,#2322,#2323));
#960=EDGE_LOOP('',(#2324,#2325,#2326,#2327));
#961=EDGE_LOOP('',(#2328,#2329,#2330,#2331));
#962=EDGE_LOOP('',(#2332,#2333,#2334,#2335));
#963=EDGE_LOOP('',(#2336,#2337,#2338,#2339,#2340,#2341));
#964=EDGE_LOOP('',(#2342,#2343,#2344,#2345,#2346,#2347,#2348,#2349,#2350,
#2351,#2352,#2353,#2354,#2355,#2356,#2357,#2358,#2359,#2360,#2361,#2362,
#2363,#2364,#2365,#2366,#2367,#2368,#2369,#2370,#2371,#2372,#2373,#2374,
#2375,#2376,#2377,#2378,#2379,#2380,#2381,#2382,#2383,#2384,#2385,#2386,
#2387,#2388,#2389,#2390,#2391,#2392,#2393,#2394,#2395));
#965=EDGE_LOOP('',(#2396,#2397,#2398,#2399));
#966=EDGE_LOOP('',(#2400));
#967=EDGE_LOOP('',(#2401));
#968=EDGE_LOOP('',(#2402,#2403,#2404,#2405));
#1103=CIRCLE('',#3338,10.5057959473896);
#1104=CIRCLE('',#3339,0.5);
#1105=CIRCLE('',#3340,10.0057959473896);
#1106=CIRCLE('',#3342,9.50579594738959);
#1107=CIRCLE('',#3344,10.5057959473896);
#1108=CIRCLE('',#3370,10.5246348408465);
#1109=CIRCLE('',#3371,11.0246348408465);
#1110=CIRCLE('',#3372,11.0246348408465);
#1111=CIRCLE('',#3373,11.0246348408465);
#1112=CIRCLE('',#3374,11.0246348408465);
#1113=CIRCLE('',#3375,11.0246348408465);
#1114=CIRCLE('',#3376,11.0246348408465);
#1115=CIRCLE('',#3377,11.0246348408465);
#1116=CIRCLE('',#3378,11.0246348408465);
#1117=CIRCLE('',#3379,11.0246348408465);
#1118=CIRCLE('',#3380,11.0246348408465);
#1119=CIRCLE('',#3381,11.0246348408465);
#1120=CIRCLE('',#3382,11.0246348408465);
#1121=CIRCLE('',#3383,11.0246348408465);
#1122=CIRCLE('',#3384,11.0246348408465);
#1123=CIRCLE('',#3385,11.0246348408465);
#1124=CIRCLE('',#3386,11.0246348408465);
#1125=CIRCLE('',#3387,11.0246348408465);
#1126=CIRCLE('',#3388,11.0246348408465);
#1127=CIRCLE('',#3389,11.0246348408465);
#1128=CIRCLE('',#3390,11.0246348408465);
#1129=CIRCLE('',#3391,11.0246348408465);
#1130=CIRCLE('',#3392,11.0246348408465);
#1131=CIRCLE('',#3393,11.0246348408465);
#1132=CIRCLE('',#3394,11.0246348408465);
#1133=CIRCLE('',#3395,11.0246348408465);
#1134=CIRCLE('',#3397,11.0246348408465);
#1135=CIRCLE('',#3399,11.0246348408465);
#1136=CIRCLE('',#3401,11.0246348408465);
#1137=CIRCLE('',#3403,11.0246348408465);
#1138=CIRCLE('',#3405,11.0246348408465);
#1139=CIRCLE('',#3407,11.0246348408465);
#1140=CIRCLE('',#3409,11.0246348408465);
#1141=CIRCLE('',#3411,11.0246348408465);
#1142=CIRCLE('',#3413,11.0246348408465);
#1143=CIRCLE('',#3415,11.0246348408465);
#1144=CIRCLE('',#3417,11.0246348408465);
#1145=CIRCLE('',#3419,11.0246348408465);
#1146=CIRCLE('',#3421,11.0246348408465);
#1147=CIRCLE('',#3423,11.0246348408465);
#1148=CIRCLE('',#3425,11.0246348408465);
#1149=CIRCLE('',#3427,11.0246348408465);
#1150=CIRCLE('',#3429,11.0246348408465);
#1151=CIRCLE('',#3431,11.0246348408465);
#1152=CIRCLE('',#3433,11.0246348408465);
#1153=CIRCLE('',#3435,11.0246348408465);
#1154=CIRCLE('',#3437,11.0246348408465);
#1155=CIRCLE('',#3439,11.0246348408465);
#1156=CIRCLE('',#3441,11.0246348408465);
#1157=CIRCLE('',#3443,11.0246348408465);
#1158=CIRCLE('',#3446,11.0246348408465);
#1159=CIRCLE('',#3450,9.50579594738959);
#1289=VERTEX_POINT('',#4665);
#1290=VERTEX_POINT('',#4667);
#1291=VERTEX_POINT('',#4671);
#1292=VERTEX_POINT('',#4674);
#1293=VERTEX_POINT('',#4678);
#1294=VERTEX_POINT('',#4679);
#1295=VERTEX_POINT('',#4694);
#1296=VERTEX_POINT('',#4696);
#1297=VERTEX_POINT('',#4713);
#1298=VERTEX_POINT('',#4714);
#1299=VERTEX_POINT('',#4729);
#1300=VERTEX_POINT('',#4731);
#1301=VERTEX_POINT('',#4748);
#1302=VERTEX_POINT('',#4749);
#1303=VERTEX_POINT('',#4764);
#1304=VERTEX_POINT('',#4766);
#1305=VERTEX_POINT('',#4783);
#1306=VERTEX_POINT('',#4784);
#1307=VERTEX_POINT('',#4799);
#1308=VERTEX_POINT('',#4801);
#1309=VERTEX_POINT('',#4818);
#1310=VERTEX_POINT('',#4819);
#1311=VERTEX_POINT('',#4834);
#1312=VERTEX_POINT('',#4836);
#1313=VERTEX_POINT('',#4853);
#1314=VERTEX_POINT('',#4854);
#1315=VERTEX_POINT('',#4869);
#1316=VERTEX_POINT('',#4871);
#1317=VERTEX_POINT('',#4888);
#1318=VERTEX_POINT('',#4889);
#1319=VERTEX_POINT('',#4904);
#1320=VERTEX_POINT('',#4906);
#1321=VERTEX_POINT('',#4923);
#1322=VERTEX_POINT('',#4924);
#1323=VERTEX_POINT('',#4939);
#1324=VERTEX_POINT('',#4941);
#1325=VERTEX_POINT('',#4958);
#1326=VERTEX_POINT('',#4959);
#1327=VERTEX_POINT('',#4974);
#1328=VERTEX_POINT('',#4976);
#1329=VERTEX_POINT('',#4993);
#1330=VERTEX_POINT('',#4994);
#1331=VERTEX_POINT('',#5009);
#1332=VERTEX_POINT('',#5011);
#1333=VERTEX_POINT('',#5028);
#1334=VERTEX_POINT('',#5029);
#1335=VERTEX_POINT('',#5044);
#1336=VERTEX_POINT('',#5046);
#1337=VERTEX_POINT('',#5063);
#1338=VERTEX_POINT('',#5064);
#1339=VERTEX_POINT('',#5079);
#1340=VERTEX_POINT('',#5081);
#1341=VERTEX_POINT('',#5098);
#1342=VERTEX_POINT('',#5099);
#1343=VERTEX_POINT('',#5114);
#1344=VERTEX_POINT('',#5116);
#1345=VERTEX_POINT('',#5133);
#1346=VERTEX_POINT('',#5134);
#1347=VERTEX_POINT('',#5149);
#1348=VERTEX_POINT('',#5151);
#1349=VERTEX_POINT('',#5168);
#1350=VERTEX_POINT('',#5169);
#1351=VERTEX_POINT('',#5184);
#1352=VERTEX_POINT('',#5186);
#1353=VERTEX_POINT('',#5203);
#1354=VERTEX_POINT('',#5204);
#1355=VERTEX_POINT('',#5219);
#1356=VERTEX_POINT('',#5221);
#1357=VERTEX_POINT('',#5238);
#1358=VERTEX_POINT('',#5239);
#1359=VERTEX_POINT('',#5254);
#1360=VERTEX_POINT('',#5256);
#1361=VERTEX_POINT('',#5273);
#1362=VERTEX_POINT('',#5274);
#1363=VERTEX_POINT('',#5289);
#1364=VERTEX_POINT('',#5291);
#1365=VERTEX_POINT('',#5308);
#1366=VERTEX_POINT('',#5309);
#1367=VERTEX_POINT('',#5324);
#1368=VERTEX_POINT('',#5326);
#1369=VERTEX_POINT('',#5343);
#1370=VERTEX_POINT('',#5344);
#1371=VERTEX_POINT('',#5359);
#1372=VERTEX_POINT('',#5361);
#1373=VERTEX_POINT('',#5378);
#1374=VERTEX_POINT('',#5379);
#1375=VERTEX_POINT('',#5394);
#1376=VERTEX_POINT('',#5396);
#1377=VERTEX_POINT('',#5413);
#1378=VERTEX_POINT('',#5414);
#1379=VERTEX_POINT('',#5429);
#1380=VERTEX_POINT('',#5431);
#1381=VERTEX_POINT('',#5448);
#1382=VERTEX_POINT('',#5449);
#1383=VERTEX_POINT('',#5464);
#1384=VERTEX_POINT('',#5466);
#1385=VERTEX_POINT('',#5483);
#1386=VERTEX_POINT('',#5484);
#1387=VERTEX_POINT('',#5499);
#1388=VERTEX_POINT('',#5501);
#1389=VERTEX_POINT('',#5518);
#1390=VERTEX_POINT('',#5520);
#1391=VERTEX_POINT('',#5522);
#1392=VERTEX_POINT('',#5555);
#1393=VERTEX_POINT('',#5566);
#1394=VERTEX_POINT('',#5570);
#1395=VERTEX_POINT('',#5618);
#1396=VERTEX_POINT('',#5641);
#1606=EDGE_CURVE('',#1289,#1289,#1103,.T.);
#1607=EDGE_CURVE('',#1289,#1290,#1104,.T.);
#1608=EDGE_CURVE('',#1290,#1290,#1105,.T.);
#1609=EDGE_CURVE('',#1291,#1291,#1106,.T.);
#1610=EDGE_CURVE('',#1292,#1292,#1107,.T.);
#1611=EDGE_CURVE('',#1292,#1289,#229,.T.);
#1612=EDGE_CURVE('',#1293,#1294,#105,.T.);
#1613=EDGE_CURVE('',#1295,#1293,#230,.T.);
#1614=EDGE_CURVE('',#1296,#1295,#106,.T.);
#1615=EDGE_CURVE('',#1294,#1296,#231,.T.);
#1616=EDGE_CURVE('',#1297,#1298,#107,.T.);
#1617=EDGE_CURVE('',#1299,#1297,#232,.T.);
#1618=EDGE_CURVE('',#1300,#1299,#108,.T.);
#1619=EDGE_CURVE('',#1298,#1300,#233,.T.);
#1620=EDGE_CURVE('',#1301,#1302,#109,.T.);
#1621=EDGE_CURVE('',#1303,#1301,#234,.T.);
#1622=EDGE_CURVE('',#1304,#1303,#110,.T.);
#1623=EDGE_CURVE('',#1302,#1304,#235,.T.);
#1624=EDGE_CURVE('',#1305,#1306,#111,.T.);
#1625=EDGE_CURVE('',#1307,#1305,#236,.T.);
#1626=EDGE_CURVE('',#1308,#1307,#112,.T.);
#1627=EDGE_CURVE('',#1306,#1308,#237,.T.);
#1628=EDGE_CURVE('',#1309,#1310,#113,.T.);
#1629=EDGE_CURVE('',#1311,#1309,#238,.T.);
#1630=EDGE_CURVE('',#1312,#1311,#114,.T.);
#1631=EDGE_CURVE('',#1310,#1312,#239,.T.);
#1632=EDGE_CURVE('',#1313,#1314,#115,.T.);
#1633=EDGE_CURVE('',#1315,#1313,#240,.T.);
#1634=EDGE_CURVE('',#1316,#1315,#116,.T.);
#1635=EDGE_CURVE('',#1314,#1316,#241,.T.);
#1636=EDGE_CURVE('',#1317,#1318,#117,.T.);
#1637=EDGE_CURVE('',#1319,#1317,#242,.T.);
#1638=EDGE_CURVE('',#1320,#1319,#118,.T.);
#1639=EDGE_CURVE('',#1318,#1320,#243,.T.);
#1640=EDGE_CURVE('',#1321,#1322,#119,.T.);
#1641=EDGE_CURVE('',#1323,#1321,#244,.T.);
#1642=EDGE_CURVE('',#1324,#1323,#120,.T.);
#1643=EDGE_CURVE('',#1322,#1324,#245,.T.);
#1644=EDGE_CURVE('',#1325,#1326,#121,.T.);
#1645=EDGE_CURVE('',#1327,#1325,#246,.T.);
#1646=EDGE_CURVE('',#1328,#1327,#122,.T.);
#1647=EDGE_CURVE('',#1326,#1328,#247,.T.);
#1648=EDGE_CURVE('',#1329,#1330,#123,.T.);
#1649=EDGE_CURVE('',#1331,#1329,#248,.T.);
#1650=EDGE_CURVE('',#1332,#1331,#124,.T.);
#1651=EDGE_CURVE('',#1330,#1332,#249,.T.);
#1652=EDGE_CURVE('',#1333,#1334,#125,.T.);
#1653=EDGE_CURVE('',#1335,#1333,#250,.T.);
#1654=EDGE_CURVE('',#1336,#1335,#126,.T.);
#1655=EDGE_CURVE('',#1334,#1336,#251,.T.);
#1656=EDGE_CURVE('',#1337,#1338,#127,.T.);
#1657=EDGE_CURVE('',#1339,#1337,#252,.T.);
#1658=EDGE_CURVE('',#1340,#1339,#128,.T.);
#1659=EDGE_CURVE('',#1338,#1340,#253,.T.);
#1660=EDGE_CURVE('',#1341,#1342,#129,.T.);
#1661=EDGE_CURVE('',#1343,#1341,#254,.T.);
#1662=EDGE_CURVE('',#1344,#1343,#130,.T.);
#1663=EDGE_CURVE('',#1342,#1344,#255,.T.);
#1664=EDGE_CURVE('',#1345,#1346,#131,.T.);
#1665=EDGE_CURVE('',#1347,#1345,#256,.T.);
#1666=EDGE_CURVE('',#1348,#1347,#132,.T.);
#1667=EDGE_CURVE('',#1346,#1348,#257,.T.);
#1668=EDGE_CURVE('',#1349,#1350,#133,.T.);
#1669=EDGE_CURVE('',#1351,#1349,#258,.T.);
#1670=EDGE_CURVE('',#1352,#1351,#134,.T.);
#1671=EDGE_CURVE('',#1350,#1352,#259,.T.);
#1672=EDGE_CURVE('',#1353,#1354,#135,.T.);
#1673=EDGE_CURVE('',#1355,#1353,#260,.T.);
#1674=EDGE_CURVE('',#1356,#1355,#136,.T.);
#1675=EDGE_CURVE('',#1354,#1356,#261,.T.);
#1676=EDGE_CURVE('',#1357,#1358,#137,.T.);
#1677=EDGE_CURVE('',#1359,#1357,#262,.T.);
#1678=EDGE_CURVE('',#1360,#1359,#138,.T.);
#1679=EDGE_CURVE('',#1358,#1360,#263,.T.);
#1680=EDGE_CURVE('',#1361,#1362,#139,.T.);
#1681=EDGE_CURVE('',#1363,#1361,#264,.T.);
#1682=EDGE_CURVE('',#1364,#1363,#140,.T.);
#1683=EDGE_CURVE('',#1362,#1364,#265,.T.);
#1684=EDGE_CURVE('',#1365,#1366,#141,.T.);
#1685=EDGE_CURVE('',#1367,#1365,#266,.T.);
#1686=EDGE_CURVE('',#1368,#1367,#142,.T.);
#1687=EDGE_CURVE('',#1366,#1368,#267,.T.);
#1688=EDGE_CURVE('',#1369,#1370,#143,.T.);
#1689=EDGE_CURVE('',#1371,#1369,#268,.T.);
#1690=EDGE_CURVE('',#1372,#1371,#144,.T.);
#1691=EDGE_CURVE('',#1370,#1372,#269,.T.);
#1692=EDGE_CURVE('',#1373,#1374,#145,.T.);
#1693=EDGE_CURVE('',#1375,#1373,#270,.T.);
#1694=EDGE_CURVE('',#1376,#1375,#146,.T.);
#1695=EDGE_CURVE('',#1374,#1376,#271,.T.);
#1696=EDGE_CURVE('',#1377,#1378,#147,.T.);
#1697=EDGE_CURVE('',#1379,#1377,#272,.T.);
#1698=EDGE_CURVE('',#1380,#1379,#148,.T.);
#1699=EDGE_CURVE('',#1378,#1380,#273,.T.);
#1700=EDGE_CURVE('',#1381,#1382,#149,.T.);
#1701=EDGE_CURVE('',#1383,#1381,#274,.T.);
#1702=EDGE_CURVE('',#1384,#1383,#150,.T.);
#1703=EDGE_CURVE('',#1382,#1384,#275,.T.);
#1704=EDGE_CURVE('',#1385,#1386,#151,.T.);
#1705=EDGE_CURVE('',#1387,#1385,#276,.T.);
#1706=EDGE_CURVE('',#1388,#1387,#152,.T.);
#1707=EDGE_CURVE('',#1386,#1388,#277,.T.);
#1708=EDGE_CURVE('',#1389,#1389,#1108,.T.);
#1709=EDGE_CURVE('',#1389,#1390,#278,.T.);
#1710=EDGE_CURVE('',#1390,#1391,#153,.T.);
#1711=EDGE_CURVE('',#1391,#1388,#1109,.T.);
#1712=EDGE_CURVE('',#1387,#1384,#1110,.T.);
#1713=EDGE_CURVE('',#1383,#1380,#1111,.T.);
#1714=EDGE_CURVE('',#1379,#1376,#1112,.T.);
#1715=EDGE_CURVE('',#1375,#1372,#1113,.T.);
#1716=EDGE_CURVE('',#1371,#1368,#1114,.T.);
#1717=EDGE_CURVE('',#1367,#1364,#1115,.T.);
#1718=EDGE_CURVE('',#1363,#1360,#1116,.T.);
#1719=EDGE_CURVE('',#1359,#1356,#1117,.T.);
#1720=EDGE_CURVE('',#1355,#1352,#1118,.T.);
#1721=EDGE_CURVE('',#1351,#1348,#1119,.T.);
#1722=EDGE_CURVE('',#1347,#1344,#1120,.T.);
#1723=EDGE_CURVE('',#1343,#1340,#1121,.T.);
#1724=EDGE_CURVE('',#1339,#1336,#1122,.T.);
#1725=EDGE_CURVE('',#1335,#1332,#1123,.T.);
#1726=EDGE_CURVE('',#1331,#1328,#1124,.T.);
#1727=EDGE_CURVE('',#1327,#1324,#1125,.T.);
#1728=EDGE_CURVE('',#1323,#1320,#1126,.T.);
#1729=EDGE_CURVE('',#1319,#1316,#1127,.T.);
#1730=EDGE_CURVE('',#1315,#1312,#1128,.T.);
#1731=EDGE_CURVE('',#1311,#1308,#1129,.T.);
#1732=EDGE_CURVE('',#1307,#1304,#1130,.T.);
#1733=EDGE_CURVE('',#1303,#1300,#1131,.T.);
#1734=EDGE_CURVE('',#1299,#1296,#1132,.T.);
#1735=EDGE_CURVE('',#1295,#1392,#1133,.T.);
#1736=EDGE_CURVE('',#1392,#1390,#154,.T.);
#1737=EDGE_CURVE('',#1293,#1393,#1134,.T.);
#1738=EDGE_CURVE('',#1393,#1392,#279,.T.);
#1739=EDGE_CURVE('',#1391,#1394,#280,.T.);
#1740=EDGE_CURVE('',#1394,#1386,#1135,.T.);
#1741=EDGE_CURVE('',#1385,#1382,#1136,.T.);
#1742=EDGE_CURVE('',#1381,#1378,#1137,.T.);
#1743=EDGE_CURVE('',#1377,#1374,#1138,.T.);
#1744=EDGE_CURVE('',#1373,#1370,#1139,.T.);
#1745=EDGE_CURVE('',#1369,#1366,#1140,.T.);
#1746=EDGE_CURVE('',#1365,#1362,#1141,.T.);
#1747=EDGE_CURVE('',#1361,#1358,#1142,.T.);
#1748=EDGE_CURVE('',#1357,#1354,#1143,.T.);
#1749=EDGE_CURVE('',#1353,#1350,#1144,.T.);
#1750=EDGE_CURVE('',#1349,#1346,#1145,.T.);
#1751=EDGE_CURVE('',#1345,#1342,#1146,.T.);
#1752=EDGE_CURVE('',#1341,#1338,#1147,.T.);
#1753=EDGE_CURVE('',#1337,#1334,#1148,.T.);
#1754=EDGE_CURVE('',#1333,#1330,#1149,.T.);
#1755=EDGE_CURVE('',#1329,#1326,#1150,.T.);
#1756=EDGE_CURVE('',#1325,#1322,#1151,.T.);
#1757=EDGE_CURVE('',#1321,#1318,#1152,.T.);
#1758=EDGE_CURVE('',#1317,#1314,#1153,.T.);
#1759=EDGE_CURVE('',#1313,#1310,#1154,.T.);
#1760=EDGE_CURVE('',#1309,#1306,#1155,.T.);
#1761=EDGE_CURVE('',#1305,#1302,#1156,.T.);
#1762=EDGE_CURVE('',#1301,#1298,#1157,.T.);
#1763=EDGE_CURVE('',#1394,#1395,#155,.T.);
#1764=EDGE_CURVE('',#1395,#1393,#156,.T.);
#1765=EDGE_CURVE('',#1297,#1294,#1158,.T.);
#1766=EDGE_CURVE('',#1395,#1292,#281,.T.);
#1767=EDGE_CURVE('',#1396,#1396,#1159,.T.);
#1768=EDGE_CURVE('',#1396,#1291,#282,.T.);
#2080=ORIENTED_EDGE('',*,*,#1606,.T.);
#2081=ORIENTED_EDGE('',*,*,#1607,.T.);
#2082=ORIENTED_EDGE('',*,*,#1608,.T.);
#2083=ORIENTED_EDGE('',*,*,#1607,.F.);
#2084=ORIENTED_EDGE('',*,*,#1608,.F.);
#2085=ORIENTED_EDGE('',*,*,#1609,.T.);
#2086=ORIENTED_EDGE('',*,*,#1610,.F.);
#2087=ORIENTED_EDGE('',*,*,#1611,.T.);
#2088=ORIENTED_EDGE('',*,*,#1606,.F.);
#2089=ORIENTED_EDGE('',*,*,#1611,.F.);
#2090=ORIENTED_EDGE('',*,*,#1612,.F.);
#2091=ORIENTED_EDGE('',*,*,#1613,.F.);
#2092=ORIENTED_EDGE('',*,*,#1614,.F.);
#2093=ORIENTED_EDGE('',*,*,#1615,.F.);
#2094=ORIENTED_EDGE('',*,*,#1616,.F.);
#2095=ORIENTED_EDGE('',*,*,#1617,.F.);
#2096=ORIENTED_EDGE('',*,*,#1618,.F.);
#2097=ORIENTED_EDGE('',*,*,#1619,.F.);
#2098=ORIENTED_EDGE('',*,*,#1620,.F.);
#2099=ORIENTED_EDGE('',*,*,#1621,.F.);
#2100=ORIENTED_EDGE('',*,*,#1622,.F.);
#2101=ORIENTED_EDGE('',*,*,#1623,.F.);
#2102=ORIENTED_EDGE('',*,*,#1624,.F.);
#2103=ORIENTED_EDGE('',*,*,#1625,.F.);
#2104=ORIENTED_EDGE('',*,*,#1626,.F.);
#2105=ORIENTED_EDGE('',*,*,#1627,.F.);
#2106=ORIENTED_EDGE('',*,*,#1628,.F.);
#2107=ORIENTED_EDGE('',*,*,#1629,.F.);
#2108=ORIENTED_EDGE('',*,*,#1630,.F.);
#2109=ORIENTED_EDGE('',*,*,#1631,.F.);
#2110=ORIENTED_EDGE('',*,*,#1632,.F.);
#2111=ORIENTED_EDGE('',*,*,#1633,.F.);
#2112=ORIENTED_EDGE('',*,*,#1634,.F.);
#2113=ORIENTED_EDGE('',*,*,#1635,.F.);
#2114=ORIENTED_EDGE('',*,*,#1636,.F.);
#2115=ORIENTED_EDGE('',*,*,#1637,.F.);
#2116=ORIENTED_EDGE('',*,*,#1638,.F.);
#2117=ORIENTED_EDGE('',*,*,#1639,.F.);
#2118=ORIENTED_EDGE('',*,*,#1640,.F.);
#2119=ORIENTED_EDGE('',*,*,#1641,.F.);
#2120=ORIENTED_EDGE('',*,*,#1642,.F.);
#2121=ORIENTED_EDGE('',*,*,#1643,.F.);
#2122=ORIENTED_EDGE('',*,*,#1644,.F.);
#2123=ORIENTED_EDGE('',*,*,#1645,.F.);
#2124=ORIENTED_EDGE('',*,*,#1646,.F.);
#2125=ORIENTED_EDGE('',*,*,#1647,.F.);
#2126=ORIENTED_EDGE('',*,*,#1648,.F.);
#2127=ORIENTED_EDGE('',*,*,#1649,.F.);
#2128=ORIENTED_EDGE('',*,*,#1650,.F.);
#2129=ORIENTED_EDGE('',*,*,#1651,.F.);
#2130=ORIENTED_EDGE('',*,*,#1652,.F.);
#2131=ORIENTED_EDGE('',*,*,#1653,.F.);
#2132=ORIENTED_EDGE('',*,*,#1654,.F.);
#2133=ORIENTED_EDGE('',*,*,#1655,.F.);
#2134=ORIENTED_EDGE('',*,*,#1656,.F.);
#2135=ORIENTED_EDGE('',*,*,#1657,.F.);
#2136=ORIENTED_EDGE('',*,*,#1658,.F.);
#2137=ORIENTED_EDGE('',*,*,#1659,.F.);
#2138=ORIENTED_EDGE('',*,*,#1660,.F.);
#2139=ORIENTED_EDGE('',*,*,#1661,.F.);
#2140=ORIENTED_EDGE('',*,*,#1662,.F.);
#2141=ORIENTED_EDGE('',*,*,#1663,.F.);
#2142=ORIENTED_EDGE('',*,*,#1664,.F.);
#2143=ORIENTED_EDGE('',*,*,#1665,.F.);
#2144=ORIENTED_EDGE('',*,*,#1666,.F.);
#2145=ORIENTED_EDGE('',*,*,#1667,.F.);
#2146=ORIENTED_EDGE('',*,*,#1668,.F.);
#2147=ORIENTED_EDGE('',*,*,#1669,.F.);
#2148=ORIENTED_EDGE('',*,*,#1670,.F.);
#2149=ORIENTED_EDGE('',*,*,#1671,.F.);
#2150=ORIENTED_EDGE('',*,*,#1672,.F.);
#2151=ORIENTED_EDGE('',*,*,#1673,.F.);
#2152=ORIENTED_EDGE('',*,*,#1674,.F.);
#2153=ORIENTED_EDGE('',*,*,#1675,.F.);
#2154=ORIENTED_EDGE('',*,*,#1676,.F.);
#2155=ORIENTED_EDGE('',*,*,#1677,.F.);
#2156=ORIENTED_EDGE('',*,*,#1678,.F.);
#2157=ORIENTED_EDGE('',*,*,#1679,.F.);
#2158=ORIENTED_EDGE('',*,*,#1680,.F.);
#2159=ORIENTED_EDGE('',*,*,#1681,.F.);
#2160=ORIENTED_EDGE('',*,*,#1682,.F.);
#2161=ORIENTED_EDGE('',*,*,#1683,.F.);
#2162=ORIENTED_EDGE('',*,*,#1684,.F.);
#2163=ORIENTED_EDGE('',*,*,#1685,.F.);
#2164=ORIENTED_EDGE('',*,*,#1686,.F.);
#2165=ORIENTED_EDGE('',*,*,#1687,.F.);
#2166=ORIENTED_EDGE('',*,*,#1688,.F.);
#2167=ORIENTED_EDGE('',*,*,#1689,.F.);
#2168=ORIENTED_EDGE('',*,*,#1690,.F.);
#2169=ORIENTED_EDGE('',*,*,#1691,.F.);
#2170=ORIENTED_EDGE('',*,*,#1692,.F.);
#2171=ORIENTED_EDGE('',*,*,#1693,.F.);
#2172=ORIENTED_EDGE('',*,*,#1694,.F.);
#2173=ORIENTED_EDGE('',*,*,#1695,.F.);
#2174=ORIENTED_EDGE('',*,*,#1696,.F.);
#2175=ORIENTED_EDGE('',*,*,#1697,.F.);
#2176=ORIENTED_EDGE('',*,*,#1698,.F.);
#2177=ORIENTED_EDGE('',*,*,#1699,.F.);
#2178=ORIENTED_EDGE('',*,*,#1700,.F.);
#2179=ORIENTED_EDGE('',*,*,#1701,.F.);
#2180=ORIENTED_EDGE('',*,*,#1702,.F.);
#2181=ORIENTED_EDGE('',*,*,#1703,.F.);
#2182=ORIENTED_EDGE('',*,*,#1704,.F.);
#2183=ORIENTED_EDGE('',*,*,#1705,.F.);
#2184=ORIENTED_EDGE('',*,*,#1706,.F.);
#2185=ORIENTED_EDGE('',*,*,#1707,.F.);
#2186=ORIENTED_EDGE('',*,*,#1708,.F.);
#2187=ORIENTED_EDGE('',*,*,#1709,.T.);
#2188=ORIENTED_EDGE('',*,*,#1710,.T.);
#2189=ORIENTED_EDGE('',*,*,#1711,.T.);
#2190=ORIENTED_EDGE('',*,*,#1706,.T.);
#2191=ORIENTED_EDGE('',*,*,#1712,.T.);
#2192=ORIENTED_EDGE('',*,*,#1702,.T.);
#2193=ORIENTED_EDGE('',*,*,#1713,.T.);
#2194=ORIENTED_EDGE('',*,*,#1698,.T.);
#2195=ORIENTED_EDGE('',*,*,#1714,.T.);
#2196=ORIENTED_EDGE('',*,*,#1694,.T.);
#2197=ORIENTED_EDGE('',*,*,#1715,.T.);
#2198=ORIENTED_EDGE('',*,*,#1690,.T.);
#2199=ORIENTED_EDGE('',*,*,#1716,.T.);
#2200=ORIENTED_EDGE('',*,*,#1686,.T.);
#2201=ORIENTED_EDGE('',*,*,#1717,.T.);
#2202=ORIENTED_EDGE('',*,*,#1682,.T.);
#2203=ORIENTED_EDGE('',*,*,#1718,.T.);
#2204=ORIENTED_EDGE('',*,*,#1678,.T.);
#2205=ORIENTED_EDGE('',*,*,#1719,.T.);
#2206=ORIENTED_EDGE('',*,*,#1674,.T.);
#2207=ORIENTED_EDGE('',*,*,#1720,.T.);
#2208=ORIENTED_EDGE('',*,*,#1670,.T.);
#2209=ORIENTED_EDGE('',*,*,#1721,.T.);
#2210=ORIENTED_EDGE('',*,*,#1666,.T.);
#2211=ORIENTED_EDGE('',*,*,#1722,.T.);
#2212=ORIENTED_EDGE('',*,*,#1662,.T.);
#2213=ORIENTED_EDGE('',*,*,#1723,.T.);
#2214=ORIENTED_EDGE('',*,*,#1658,.T.);
#2215=ORIENTED_EDGE('',*,*,#1724,.T.);
#2216=ORIENTED_EDGE('',*,*,#1654,.T.);
#2217=ORIENTED_EDGE('',*,*,#1725,.T.);
#2218=ORIENTED_EDGE('',*,*,#1650,.T.);
#2219=ORIENTED_EDGE('',*,*,#1726,.T.);
#2220=ORIENTED_EDGE('',*,*,#1646,.T.);
#2221=ORIENTED_EDGE('',*,*,#1727,.T.);
#2222=ORIENTED_EDGE('',*,*,#1642,.T.);
#2223=ORIENTED_EDGE('',*,*,#1728,.T.);
#2224=ORIENTED_EDGE('',*,*,#1638,.T.);
#2225=ORIENTED_EDGE('',*,*,#1729,.T.);
#2226=ORIENTED_EDGE('',*,*,#1634,.T.);
#2227=ORIENTED_EDGE('',*,*,#1730,.T.);
#2228=ORIENTED_EDGE('',*,*,#1630,.T.);
#2229=ORIENTED_EDGE('',*,*,#1731,.T.);
#2230=ORIENTED_EDGE('',*,*,#1626,.T.);
#2231=ORIENTED_EDGE('',*,*,#1732,.T.);
#2232=ORIENTED_EDGE('',*,*,#1622,.T.);
#2233=ORIENTED_EDGE('',*,*,#1733,.T.);
#2234=ORIENTED_EDGE('',*,*,#1618,.T.);
#2235=ORIENTED_EDGE('',*,*,#1734,.T.);
#2236=ORIENTED_EDGE('',*,*,#1614,.T.);
#2237=ORIENTED_EDGE('',*,*,#1735,.T.);
#2238=ORIENTED_EDGE('',*,*,#1736,.T.);
#2239=ORIENTED_EDGE('',*,*,#1709,.F.);
#2240=ORIENTED_EDGE('',*,*,#1613,.T.);
#2241=ORIENTED_EDGE('',*,*,#1737,.T.);
#2242=ORIENTED_EDGE('',*,*,#1738,.T.);
#2243=ORIENTED_EDGE('',*,*,#1735,.F.);
#2244=ORIENTED_EDGE('',*,*,#1707,.T.);
#2245=ORIENTED_EDGE('',*,*,#1711,.F.);
#2246=ORIENTED_EDGE('',*,*,#1739,.T.);
#2247=ORIENTED_EDGE('',*,*,#1740,.T.);
#2248=ORIENTED_EDGE('',*,*,#1703,.T.);
#2249=ORIENTED_EDGE('',*,*,#1712,.F.);
#2250=ORIENTED_EDGE('',*,*,#1705,.T.);
#2251=ORIENTED_EDGE('',*,*,#1741,.T.);
#2252=ORIENTED_EDGE('',*,*,#1699,.T.);
#2253=ORIENTED_EDGE('',*,*,#1713,.F.);
#2254=ORIENTED_EDGE('',*,*,#1701,.T.);
#2255=ORIENTED_EDGE('',*,*,#1742,.T.);
#2256=ORIENTED_EDGE('',*,*,#1695,.T.);
#2257=ORIENTED_EDGE('',*,*,#1714,.F.);
#2258=ORIENTED_EDGE('',*,*,#1697,.T.);
#2259=ORIENTED_EDGE('',*,*,#1743,.T.);
#2260=ORIENTED_EDGE('',*,*,#1691,.T.);
#2261=ORIENTED_EDGE('',*,*,#1715,.F.);
#2262=ORIENTED_EDGE('',*,*,#1693,.T.);
#2263=ORIENTED_EDGE('',*,*,#1744,.T.);
#2264=ORIENTED_EDGE('',*,*,#1687,.T.);
#2265=ORIENTED_EDGE('',*,*,#1716,.F.);
#2266=ORIENTED_EDGE('',*,*,#1689,.T.);
#2267=ORIENTED_EDGE('',*,*,#1745,.T.);
#2268=ORIENTED_EDGE('',*,*,#1683,.T.);
#2269=ORIENTED_EDGE('',*,*,#1717,.F.);
#2270=ORIENTED_EDGE('',*,*,#1685,.T.);
#2271=ORIENTED_EDGE('',*,*,#1746,.T.);
#2272=ORIENTED_EDGE('',*,*,#1679,.T.);
#2273=ORIENTED_EDGE('',*,*,#1718,.F.);
#2274=ORIENTED_EDGE('',*,*,#1681,.T.);
#2275=ORIENTED_EDGE('',*,*,#1747,.T.);
#2276=ORIENTED_EDGE('',*,*,#1675,.T.);
#2277=ORIENTED_EDGE('',*,*,#1719,.F.);
#2278=ORIENTED_EDGE('',*,*,#1677,.T.);
#2279=ORIENTED_EDGE('',*,*,#1748,.T.);
#2280=ORIENTED_EDGE('',*,*,#1671,.T.);
#2281=ORIENTED_EDGE('',*,*,#1720,.F.);
#2282=ORIENTED_EDGE('',*,*,#1673,.T.);
#2283=ORIENTED_EDGE('',*,*,#1749,.T.);
#2284=ORIENTED_EDGE('',*,*,#1667,.T.);
#2285=ORIENTED_EDGE('',*,*,#1721,.F.);
#2286=ORIENTED_EDGE('',*,*,#1669,.T.);
#2287=ORIENTED_EDGE('',*,*,#1750,.T.);
#2288=ORIENTED_EDGE('',*,*,#1663,.T.);
#2289=ORIENTED_EDGE('',*,*,#1722,.F.);
#2290=ORIENTED_EDGE('',*,*,#1665,.T.);
#2291=ORIENTED_EDGE('',*,*,#1751,.T.);
#2292=ORIENTED_EDGE('',*,*,#1659,.T.);
#2293=ORIENTED_EDGE('',*,*,#1723,.F.);
#2294=ORIENTED_EDGE('',*,*,#1661,.T.);
#2295=ORIENTED_EDGE('',*,*,#1752,.T.);
#2296=ORIENTED_EDGE('',*,*,#1655,.T.);
#2297=ORIENTED_EDGE('',*,*,#1724,.F.);
#2298=ORIENTED_EDGE('',*,*,#1657,.T.);
#2299=ORIENTED_EDGE('',*,*,#1753,.T.);
#2300=ORIENTED_EDGE('',*,*,#1651,.T.);
#2301=ORIENTED_EDGE('',*,*,#1725,.F.);
#2302=ORIENTED_EDGE('',*,*,#1653,.T.);
#2303=ORIENTED_EDGE('',*,*,#1754,.T.);
#2304=ORIENTED_EDGE('',*,*,#1647,.T.);
#2305=ORIENTED_EDGE('',*,*,#1726,.F.);
#2306=ORIENTED_EDGE('',*,*,#1649,.T.);
#2307=ORIENTED_EDGE('',*,*,#1755,.T.);
#2308=ORIENTED_EDGE('',*,*,#1643,.T.);
#2309=ORIENTED_EDGE('',*,*,#1727,.F.);
#2310=ORIENTED_EDGE('',*,*,#1645,.T.);
#2311=ORIENTED_EDGE('',*,*,#1756,.T.);
#2312=ORIENTED_EDGE('',*,*,#1639,.T.);
#2313=ORIENTED_EDGE('',*,*,#1728,.F.);
#2314=ORIENTED_EDGE('',*,*,#1641,.T.);
#2315=ORIENTED_EDGE('',*,*,#1757,.T.);
#2316=ORIENTED_EDGE('',*,*,#1635,.T.);
#2317=ORIENTED_EDGE('',*,*,#1729,.F.);
#2318=ORIENTED_EDGE('',*,*,#1637,.T.);
#2319=ORIENTED_EDGE('',*,*,#1758,.T.);
#2320=ORIENTED_EDGE('',*,*,#1631,.T.);
#2321=ORIENTED_EDGE('',*,*,#1730,.F.);
#2322=ORIENTED_EDGE('',*,*,#1633,.T.);
#2323=ORIENTED_EDGE('',*,*,#1759,.T.);
#2324=ORIENTED_EDGE('',*,*,#1627,.T.);
#2325=ORIENTED_EDGE('',*,*,#1731,.F.);
#2326=ORIENTED_EDGE('',*,*,#1629,.T.);
#2327=ORIENTED_EDGE('',*,*,#1760,.T.);
#2328=ORIENTED_EDGE('',*,*,#1623,.T.);
#2329=ORIENTED_EDGE('',*,*,#1732,.F.);
#2330=ORIENTED_EDGE('',*,*,#1625,.T.);
#2331=ORIENTED_EDGE('',*,*,#1761,.T.);
#2332=ORIENTED_EDGE('',*,*,#1619,.T.);
#2333=ORIENTED_EDGE('',*,*,#1733,.F.);
#2334=ORIENTED_EDGE('',*,*,#1621,.T.);
#2335=ORIENTED_EDGE('',*,*,#1762,.T.);
#2336=ORIENTED_EDGE('',*,*,#1763,.F.);
#2337=ORIENTED_EDGE('',*,*,#1739,.F.);
#2338=ORIENTED_EDGE('',*,*,#1710,.F.);
#2339=ORIENTED_EDGE('',*,*,#1736,.F.);
#2340=ORIENTED_EDGE('',*,*,#1738,.F.);
#2341=ORIENTED_EDGE('',*,*,#1764,.F.);
#2342=ORIENTED_EDGE('',*,*,#1612,.T.);
#2343=ORIENTED_EDGE('',*,*,#1765,.F.);
#2344=ORIENTED_EDGE('',*,*,#1616,.T.);
#2345=ORIENTED_EDGE('',*,*,#1762,.F.);
#2346=ORIENTED_EDGE('',*,*,#1620,.T.);
#2347=ORIENTED_EDGE('',*,*,#1761,.F.);
#2348=ORIENTED_EDGE('',*,*,#1624,.T.);
#2349=ORIENTED_EDGE('',*,*,#1760,.F.);
#2350=ORIENTED_EDGE('',*,*,#1628,.T.);
#2351=ORIENTED_EDGE('',*,*,#1759,.F.);
#2352=ORIENTED_EDGE('',*,*,#1632,.T.);
#2353=ORIENTED_EDGE('',*,*,#1758,.F.);
#2354=ORIENTED_EDGE('',*,*,#1636,.T.);
#2355=ORIENTED_EDGE('',*,*,#1757,.F.);
#2356=ORIENTED_EDGE('',*,*,#1640,.T.);
#2357=ORIENTED_EDGE('',*,*,#1756,.F.);
#2358=ORIENTED_EDGE('',*,*,#1644,.T.);
#2359=ORIENTED_EDGE('',*,*,#1755,.F.);
#2360=ORIENTED_EDGE('',*,*,#1648,.T.);
#2361=ORIENTED_EDGE('',*,*,#1754,.F.);
#2362=ORIENTED_EDGE('',*,*,#1652,.T.);
#2363=ORIENTED_EDGE('',*,*,#1753,.F.);
#2364=ORIENTED_EDGE('',*,*,#1656,.T.);
#2365=ORIENTED_EDGE('',*,*,#1752,.F.);
#2366=ORIENTED_EDGE('',*,*,#1660,.T.);
#2367=ORIENTED_EDGE('',*,*,#1751,.F.);
#2368=ORIENTED_EDGE('',*,*,#1664,.T.);
#2369=ORIENTED_EDGE('',*,*,#1750,.F.);
#2370=ORIENTED_EDGE('',*,*,#1668,.T.);
#2371=ORIENTED_EDGE('',*,*,#1749,.F.);
#2372=ORIENTED_EDGE('',*,*,#1672,.T.);
#2373=ORIENTED_EDGE('',*,*,#1748,.F.);
#2374=ORIENTED_EDGE('',*,*,#1676,.T.);
#2375=ORIENTED_EDGE('',*,*,#1747,.F.);
#2376=ORIENTED_EDGE('',*,*,#1680,.T.);
#2377=ORIENTED_EDGE('',*,*,#1746,.F.);
#2378=ORIENTED_EDGE('',*,*,#1684,.T.);
#2379=ORIENTED_EDGE('',*,*,#1745,.F.);
#2380=ORIENTED_EDGE('',*,*,#1688,.T.);
#2381=ORIENTED_EDGE('',*,*,#1744,.F.);
#2382=ORIENTED_EDGE('',*,*,#1692,.T.);
#2383=ORIENTED_EDGE('',*,*,#1743,.F.);
#2384=ORIENTED_EDGE('',*,*,#1696,.T.);
#2385=ORIENTED_EDGE('',*,*,#1742,.F.);
#2386=ORIENTED_EDGE('',*,*,#1700,.T.);
#2387=ORIENTED_EDGE('',*,*,#1741,.F.);
#2388=ORIENTED_EDGE('',*,*,#1704,.T.);
#2389=ORIENTED_EDGE('',*,*,#1740,.F.);
#2390=ORIENTED_EDGE('',*,*,#1763,.T.);
#2391=ORIENTED_EDGE('',*,*,#1766,.T.);
#2392=ORIENTED_EDGE('',*,*,#1610,.T.);
#2393=ORIENTED_EDGE('',*,*,#1766,.F.);
#2394=ORIENTED_EDGE('',*,*,#1764,.T.);
#2395=ORIENTED_EDGE('',*,*,#1737,.F.);
#2396=ORIENTED_EDGE('',*,*,#1615,.T.);
#2397=ORIENTED_EDGE('',*,*,#1734,.F.);
#2398=ORIENTED_EDGE('',*,*,#1617,.T.);
#2399=ORIENTED_EDGE('',*,*,#1765,.T.);
#2400=ORIENTED_EDGE('',*,*,#1708,.T.);
#2401=ORIENTED_EDGE('',*,*,#1767,.F.);
#2402=ORIENTED_EDGE('',*,*,#1767,.T.);
#2403=ORIENTED_EDGE('',*,*,#1768,.T.);
#2404=ORIENTED_EDGE('',*,*,#1609,.F.);
#2405=ORIENTED_EDGE('',*,*,#1768,.F.);
#3028=TOROIDAL_SURFACE('',#3337,10.0057959473896,0.5);
#3032=ADVANCED_FACE('',(#728),#3028,.T.);
#3033=ADVANCED_FACE('',(#729,#689),#700,.T.);
#3034=ADVANCED_FACE('',(#730),#549,.T.);
#3035=ADVANCED_FACE('',(#731),#550,.F.);
#3036=ADVANCED_FACE('',(#732),#551,.F.);
#3037=ADVANCED_FACE('',(#733),#552,.F.);
#3038=ADVANCED_FACE('',(#734),#553,.F.);
#3039=ADVANCED_FACE('',(#735),#554,.F.);
#3040=ADVANCED_FACE('',(#736),#555,.F.);
#3041=ADVANCED_FACE('',(#737),#556,.F.);
#3042=ADVANCED_FACE('',(#738),#557,.F.);
#3043=ADVANCED_FACE('',(#739),#558,.F.);
#3044=ADVANCED_FACE('',(#740),#559,.F.);
#3045=ADVANCED_FACE('',(#741),#560,.F.);
#3046=ADVANCED_FACE('',(#742),#561,.F.);
#3047=ADVANCED_FACE('',(#743),#562,.F.);
#3048=ADVANCED_FACE('',(#744),#563,.F.);
#3049=ADVANCED_FACE('',(#745),#564,.F.);
#3050=ADVANCED_FACE('',(#746),#565,.F.);
#3051=ADVANCED_FACE('',(#747),#566,.F.);
#3052=ADVANCED_FACE('',(#748),#567,.F.);
#3053=ADVANCED_FACE('',(#749),#568,.F.);
#3054=ADVANCED_FACE('',(#750),#569,.F.);
#3055=ADVANCED_FACE('',(#751),#570,.F.);
#3056=ADVANCED_FACE('',(#752),#571,.F.);
#3057=ADVANCED_FACE('',(#753),#572,.F.);
#3058=ADVANCED_FACE('',(#754),#573,.F.);
#3059=ADVANCED_FACE('',(#755),#97,.T.);
#3060=ADVANCED_FACE('',(#756),#574,.T.);
#3061=ADVANCED_FACE('',(#757),#575,.T.);
#3062=ADVANCED_FACE('',(#758),#576,.T.);
#3063=ADVANCED_FACE('',(#759),#577,.T.);
#3064=ADVANCED_FACE('',(#760),#578,.T.);
#3065=ADVANCED_FACE('',(#761),#579,.T.);
#3066=ADVANCED_FACE('',(#762),#580,.T.);
#3067=ADVANCED_FACE('',(#763),#581,.T.);
#3068=ADVANCED_FACE('',(#764),#582,.T.);
#3069=ADVANCED_FACE('',(#765),#583,.T.);
#3070=ADVANCED_FACE('',(#766),#584,.T.);
#3071=ADVANCED_FACE('',(#767),#585,.T.);
#3072=ADVANCED_FACE('',(#768),#586,.T.);
#3073=ADVANCED_FACE('',(#769),#587,.T.);
#3074=ADVANCED_FACE('',(#770),#588,.T.);
#3075=ADVANCED_FACE('',(#771),#589,.T.);
#3076=ADVANCED_FACE('',(#772),#590,.T.);
#3077=ADVANCED_FACE('',(#773),#591,.T.);
#3078=ADVANCED_FACE('',(#774),#592,.T.);
#3079=ADVANCED_FACE('',(#775),#593,.T.);
#3080=ADVANCED_FACE('',(#776),#594,.T.);
#3081=ADVANCED_FACE('',(#777),#595,.T.);
#3082=ADVANCED_FACE('',(#778),#596,.T.);
#3083=ADVANCED_FACE('',(#779),#597,.T.);
#3084=ADVANCED_FACE('',(#780),#598,.F.);
#3085=ADVANCED_FACE('',(#781),#98,.T.);
#3086=ADVANCED_FACE('',(#782),#599,.T.);
#3087=ADVANCED_FACE('',(#783),#701,.T.);
#3088=ADVANCED_FACE('',(#784),#702,.T.);
#3089=ADVANCED_FACE('',(#785),#600,.F.);
#3214=CLOSED_SHELL('',(#3032,#3033,#3034,#3035,#3036,#3037,#3038,#3039,
#3040,#3041,#3042,#3043,#3044,#3045,#3046,#3047,#3048,#3049,#3050,#3051,
#3052,#3053,#3054,#3055,#3056,#3057,#3058,#3059,#3060,#3061,#3062,#3063,
#3064,#3065,#3066,#3067,#3068,#3069,#3070,#3071,#3072,#3073,#3074,#3075,
#3076,#3077,#3078,#3079,#3080,#3081,#3082,#3083,#3084,#3085,#3086,#3087,
#3088,#3089));
#3336=AXIS2_PLACEMENT_3D('',#4663,#3726,#3727);
#3337=AXIS2_PLACEMENT_3D('',#4664,#3728,#3729);
#3338=AXIS2_PLACEMENT_3D('',#4666,#3730,#3731);
#3339=AXIS2_PLACEMENT_3D('',#4668,#3732,#3733);
#3340=AXIS2_PLACEMENT_3D('',#4669,#3734,#3735);
#3341=AXIS2_PLACEMENT_3D('',#4670,#3736,#3737);
#3342=AXIS2_PLACEMENT_3D('',#4672,#3738,#3739);
#3343=AXIS2_PLACEMENT_3D('',#4673,#3740,#3741);
#3344=AXIS2_PLACEMENT_3D('',#4675,#3742,#3743);
#3345=AXIS2_PLACEMENT_3D('',#4677,#3745,#3746);
#3346=AXIS2_PLACEMENT_3D('',#4712,#3749,#3750);
#3347=AXIS2_PLACEMENT_3D('',#4747,#3753,#3754);
#3348=AXIS2_PLACEMENT_3D('',#4782,#3757,#3758);
#3349=AXIS2_PLACEMENT_3D('',#4817,#3761,#3762);
#3350=AXIS2_PLACEMENT_3D('',#4852,#3765,#3766);
#3351=AXIS2_PLACEMENT_3D('',#4887,#3769,#3770);
#3352=AXIS2_PLACEMENT_3D('',#4922,#3773,#3774);
#3353=AXIS2_PLACEMENT_3D('',#4957,#3777,#3778);
#3354=AXIS2_PLACEMENT_3D('',#4992,#3781,#3782);
#3355=AXIS2_PLACEMENT_3D('',#5027,#3785,#3786);
#3356=AXIS2_PLACEMENT_3D('',#5062,#3789,#3790);
#3357=AXIS2_PLACEMENT_3D('',#5097,#3793,#3794);
#3358=AXIS2_PLACEMENT_3D('',#5132,#3797,#3798);
#3359=AXIS2_PLACEMENT_3D('',#5167,#3801,#3802);
#3360=AXIS2_PLACEMENT_3D('',#5202,#3805,#3806);
#3361=AXIS2_PLACEMENT_3D('',#5237,#3809,#3810);
#3362=AXIS2_PLACEMENT_3D('',#5272,#3813,#3814);
#3363=AXIS2_PLACEMENT_3D('',#5307,#3817,#3818);
#3364=AXIS2_PLACEMENT_3D('',#5342,#3821,#3822);
#3365=AXIS2_PLACEMENT_3D('',#5377,#3825,#3826);
#3366=AXIS2_PLACEMENT_3D('',#5412,#3829,#3830);
#3367=AXIS2_PLACEMENT_3D('',#5447,#3833,#3834);
#3368=AXIS2_PLACEMENT_3D('',#5482,#3837,#3838);
#3369=AXIS2_PLACEMENT_3D('',#5517,#3841,#3842);
#3370=AXIS2_PLACEMENT_3D('',#5519,#3843,#3844);
#3371=AXIS2_PLACEMENT_3D('',#5531,#3846,#3847);
#3372=AXIS2_PLACEMENT_3D('',#5532,#3848,#3849);
#3373=AXIS2_PLACEMENT_3D('',#5533,#3850,#3851);
#3374=AXIS2_PLACEMENT_3D('',#5534,#3852,#3853);
#3375=AXIS2_PLACEMENT_3D('',#5535,#3854,#3855);
#3376=AXIS2_PLACEMENT_3D('',#5536,#3856,#3857);
#3377=AXIS2_PLACEMENT_3D('',#5537,#3858,#3859);
#3378=AXIS2_PLACEMENT_3D('',#5538,#3860,#3861);
#3379=AXIS2_PLACEMENT_3D('',#5539,#3862,#3863);
#3380=AXIS2_PLACEMENT_3D('',#5540,#3864,#3865);
#3381=AXIS2_PLACEMENT_3D('',#5541,#3866,#3867);
#3382=AXIS2_PLACEMENT_3D('',#5542,#3868,#3869);
#3383=AXIS2_PLACEMENT_3D('',#5543,#3870,#3871);
#3384=AXIS2_PLACEMENT_3D('',#5544,#3872,#3873);
#3385=AXIS2_PLACEMENT_3D('',#5545,#3874,#3875);
#3386=AXIS2_PLACEMENT_3D('',#5546,#3876,#3877);
#3387=AXIS2_PLACEMENT_3D('',#5547,#3878,#3879);
#3388=AXIS2_PLACEMENT_3D('',#5548,#3880,#3881);
#3389=AXIS2_PLACEMENT_3D('',#5549,#3882,#3883);
#3390=AXIS2_PLACEMENT_3D('',#5550,#3884,#3885);
#3391=AXIS2_PLACEMENT_3D('',#5551,#3886,#3887);
#3392=AXIS2_PLACEMENT_3D('',#5552,#3888,#3889);
#3393=AXIS2_PLACEMENT_3D('',#5553,#3890,#3891);
#3394=AXIS2_PLACEMENT_3D('',#5554,#3892,#3893);
#3395=AXIS2_PLACEMENT_3D('',#5556,#3894,#3895);
#3396=AXIS2_PLACEMENT_3D('',#5565,#3896,#3897);
#3397=AXIS2_PLACEMENT_3D('',#5567,#3898,#3899);
#3398=AXIS2_PLACEMENT_3D('',#5569,#3901,#3902);
#3399=AXIS2_PLACEMENT_3D('',#5572,#3904,#3905);
#3400=AXIS2_PLACEMENT_3D('',#5573,#3906,#3907);
#3401=AXIS2_PLACEMENT_3D('',#5574,#3908,#3909);
#3402=AXIS2_PLACEMENT_3D('',#5575,#3910,#3911);
#3403=AXIS2_PLACEMENT_3D('',#5576,#3912,#3913);
#3404=AXIS2_PLACEMENT_3D('',#5577,#3914,#3915);
#3405=AXIS2_PLACEMENT_3D('',#5578,#3916,#3917);
#3406=AXIS2_PLACEMENT_3D('',#5579,#3918,#3919);
#3407=AXIS2_PLACEMENT_3D('',#5580,#3920,#3921);
#3408=AXIS2_PLACEMENT_3D('',#5581,#3922,#3923);
#3409=AXIS2_PLACEMENT_3D('',#5582,#3924,#3925);
#3410=AXIS2_PLACEMENT_3D('',#5583,#3926,#3927);
#3411=AXIS2_PLACEMENT_3D('',#5584,#3928,#3929);
#3412=AXIS2_PLACEMENT_3D('',#5585,#3930,#3931);
#3413=AXIS2_PLACEMENT_3D('',#5586,#3932,#3933);
#3414=AXIS2_PLACEMENT_3D('',#5587,#3934,#3935);
#3415=AXIS2_PLACEMENT_3D('',#5588,#3936,#3937);
#3416=AXIS2_PLACEMENT_3D('',#5589,#3938,#3939);
#3417=AXIS2_PLACEMENT_3D('',#5590,#3940,#3941);
#3418=AXIS2_PLACEMENT_3D('',#5591,#3942,#3943);
#3419=AXIS2_PLACEMENT_3D('',#5592,#3944,#3945);
#3420=AXIS2_PLACEMENT_3D('',#5593,#3946,#3947);
#3421=AXIS2_PLACEMENT_3D('',#5594,#3948,#3949);
#3422=AXIS2_PLACEMENT_3D('',#5595,#3950,#3951);
#3423=AXIS2_PLACEMENT_3D('',#5596,#3952,#3953);
#3424=AXIS2_PLACEMENT_3D('',#5597,#3954,#3955);
#3425=AXIS2_PLACEMENT_3D('',#5598,#3956,#3957);
#3426=AXIS2_PLACEMENT_3D('',#5599,#3958,#3959);
#3427=AXIS2_PLACEMENT_3D('',#5600,#3960,#3961);
#3428=AXIS2_PLACEMENT_3D('',#5601,#3962,#3963);
#3429=AXIS2_PLACEMENT_3D('',#5602,#3964,#3965);
#3430=AXIS2_PLACEMENT_3D('',#5603,#3966,#3967);
#3431=AXIS2_PLACEMENT_3D('',#5604,#3968,#3969);
#3432=AXIS2_PLACEMENT_3D('',#5605,#3970,#3971);
#3433=AXIS2_PLACEMENT_3D('',#5606,#3972,#3973);
#3434=AXIS2_PLACEMENT_3D('',#5607,#3974,#3975);
#3435=AXIS2_PLACEMENT_3D('',#5608,#3976,#3977);
#3436=AXIS2_PLACEMENT_3D('',#5609,#3978,#3979);
#3437=AXIS2_PLACEMENT_3D('',#5610,#3980,#3981);
#3438=AXIS2_PLACEMENT_3D('',#5611,#3982,#3983);
#3439=AXIS2_PLACEMENT_3D('',#5612,#3984,#3985);
#3440=AXIS2_PLACEMENT_3D('',#5613,#3986,#3987);
#3441=AXIS2_PLACEMENT_3D('',#5614,#3988,#3989);
#3442=AXIS2_PLACEMENT_3D('',#5615,#3990,#3991);
#3443=AXIS2_PLACEMENT_3D('',#5616,#3992,#3993);
#3444=AXIS2_PLACEMENT_3D('',#5617,#3994,#3995);
#3445=AXIS2_PLACEMENT_3D('',#5635,#3996,#3997);
#3446=AXIS2_PLACEMENT_3D('',#5636,#3998,#3999);
#3447=AXIS2_PLACEMENT_3D('',#5638,#4001,#4002);
#3448=AXIS2_PLACEMENT_3D('',#5639,#4003,#4004);
#3449=AXIS2_PLACEMENT_3D('',#5640,#4005,#4006);
#3450=AXIS2_PLACEMENT_3D('',#5642,#4007,#4008);
#3451=AXIS2_PLACEMENT_3D('',#5643,#4009,#4010);
#3726=DIRECTION('axis',(0.,0.,1.));
#3727=DIRECTION('refdir',(1.,0.,0.));
#3728=DIRECTION('center_axis',(1.,0.,0.));
#3729=DIRECTION('ref_axis',(0.,0.,-1.));
#3730=DIRECTION('center_axis',(-1.,0.,0.));
#3731=DIRECTION('ref_axis',(0.,1.22464679914735E-16,1.));
#3732=DIRECTION('center_axis',(0.,-1.,-1.22464679914735E-16));
#3733=DIRECTION('ref_axis',(0.,-1.22464679914735E-16,1.));
#3734=DIRECTION('center_axis',(1.,0.,0.));
#3735=DIRECTION('ref_axis',(0.,1.22464679914735E-16,1.));
#3736=DIRECTION('center_axis',(-1.,0.,0.));
#3737=DIRECTION('ref_axis',(0.,0.,1.));
#3738=DIRECTION('center_axis',(1.,0.,0.));
#3739=DIRECTION('ref_axis',(0.,0.,-1.));
#3740=DIRECTION('center_axis',(1.,0.,0.));
#3741=DIRECTION('ref_axis',(0.,0.,-1.));
#3742=DIRECTION('center_axis',(1.,0.,0.));
#3743=DIRECTION('ref_axis',(0.,0.,-1.));
#3744=DIRECTION('',(-1.,0.,0.));
#3745=DIRECTION('center_axis',(-1.,0.,0.));
#3746=DIRECTION('ref_axis',(0.,0.968583161128631,-0.248689887164855));
#3747=DIRECTION('',(-1.,0.,0.));
#3748=DIRECTION('',(1.,0.,0.));
#3749=DIRECTION('center_axis',(-1.,0.,0.));
#3750=DIRECTION('ref_axis',(0.,0.876306680043864,-0.481753674101715));
#3751=DIRECTION('',(-1.,0.,0.));
#3752=DIRECTION('',(1.,0.,0.));
#3753=DIRECTION('center_axis',(-1.,0.,0.));
#3754=DIRECTION('ref_axis',(0.,0.728968627421412,-0.684547105928688));
#3755=DIRECTION('',(-1.,0.,0.));
#3756=DIRECTION('',(1.,0.,0.));
#3757=DIRECTION('center_axis',(-1.,0.,0.));
#3758=DIRECTION('ref_axis',(0.,0.535826794978997,-0.844327925502015));
#3759=DIRECTION('',(-1.,0.,0.));
#3760=DIRECTION('',(1.,0.,0.));
#3761=DIRECTION('center_axis',(-1.,0.,0.));
#3762=DIRECTION('ref_axis',(0.,0.309016994374947,-0.951056516295154));
#3763=DIRECTION('',(-1.,0.,0.));
#3764=DIRECTION('',(1.,0.,0.));
#3765=DIRECTION('center_axis',(-1.,0.,0.));
#3766=DIRECTION('ref_axis',(0.,0.0627905195293137,-0.998026728428272));
#3767=DIRECTION('',(-1.,0.,0.));
#3768=DIRECTION('',(1.,0.,0.));
#3769=DIRECTION('center_axis',(-1.,0.,0.));
#3770=DIRECTION('ref_axis',(0.,-0.187381314585725,-0.982287250728689));
#3771=DIRECTION('',(-1.,0.,0.));
#3772=DIRECTION('',(1.,0.,0.));
#3773=DIRECTION('center_axis',(-1.,0.,0.));
#3774=DIRECTION('ref_axis',(0.,-0.425779291565072,-0.90482705246602));
#3775=DIRECTION('',(-1.,0.,0.));
#3776=DIRECTION('',(1.,0.,0.));
#3777=DIRECTION('center_axis',(-1.,0.,0.));
#3778=DIRECTION('ref_axis',(0.,-0.637423989748689,-0.770513242775789));
#3779=DIRECTION('',(-1.,0.,0.));
#3780=DIRECTION('',(1.,0.,0.));
#3781=DIRECTION('center_axis',(-1.,0.,0.));
#3782=DIRECTION('ref_axis',(0.,-0.809016994374947,-0.587785252292473));
#3783=DIRECTION('',(-1.,0.,0.));
#3784=DIRECTION('',(1.,0.,0.));
#3785=DIRECTION('center_axis',(-1.,0.,0.));
#3786=DIRECTION('ref_axis',(0.,-0.929776485888251,-0.368124552684678));
#3787=DIRECTION('',(-1.,0.,0.));
#3788=DIRECTION('',(1.,0.,0.));
#3789=DIRECTION('center_axis',(-1.,0.,0.));
#3790=DIRECTION('ref_axis',(0.,-0.992114701314478,-0.125333233564304));
#3791=DIRECTION('',(-1.,0.,0.));
#3792=DIRECTION('',(1.,0.,0.));
#3793=DIRECTION('center_axis',(-1.,0.,0.));
#3794=DIRECTION('ref_axis',(0.,-0.992114701314478,0.125333233564304));
#3795=DIRECTION('',(-1.,0.,0.));
#3796=DIRECTION('',(1.,0.,0.));
#3797=DIRECTION('center_axis',(-1.,0.,0.));
#3798=DIRECTION('ref_axis',(0.,-0.929776485888251,0.368124552684678));
#3799=DIRECTION('',(-1.,0.,0.));
#3800=DIRECTION('',(1.,0.,0.));
#3801=DIRECTION('center_axis',(-1.,0.,0.));
#3802=DIRECTION('ref_axis',(0.,-0.809016994374947,0.587785252292473));
#3803=DIRECTION('',(-1.,0.,0.));
#3804=DIRECTION('',(1.,0.,0.));
#3805=DIRECTION('center_axis',(-1.,0.,0.));
#3806=DIRECTION('ref_axis',(0.,-0.63742398974869,0.770513242775789));
#3807=DIRECTION('',(-1.,0.,0.));
#3808=DIRECTION('',(1.,0.,0.));
#3809=DIRECTION('center_axis',(-1.,0.,0.));
#3810=DIRECTION('ref_axis',(0.,-0.425779291565073,0.904827052466019));
#3811=DIRECTION('',(-1.,0.,0.));
#3812=DIRECTION('',(1.,0.,0.));
#3813=DIRECTION('center_axis',(-1.,0.,0.));
#3814=DIRECTION('ref_axis',(0.,-0.187381314585725,0.982287250728689));
#3815=DIRECTION('',(-1.,0.,0.));
#3816=DIRECTION('',(1.,0.,0.));
#3817=DIRECTION('center_axis',(-1.,0.,0.));
#3818=DIRECTION('ref_axis',(0.,0.0627905195293132,0.998026728428272));
#3819=DIRECTION('',(-1.,0.,0.));
#3820=DIRECTION('',(1.,0.,0.));
#3821=DIRECTION('center_axis',(-1.,0.,0.));
#3822=DIRECTION('ref_axis',(0.,0.309016994374947,0.951056516295154));
#3823=DIRECTION('',(-1.,0.,0.));
#3824=DIRECTION('',(1.,0.,0.));
#3825=DIRECTION('center_axis',(-1.,0.,0.));
#3826=DIRECTION('ref_axis',(0.,0.535826794978997,0.844327925502015));
#3827=DIRECTION('',(-1.,0.,0.));
#3828=DIRECTION('',(1.,0.,0.));
#3829=DIRECTION('center_axis',(-1.,0.,0.));
#3830=DIRECTION('ref_axis',(0.,0.728968627421412,0.684547105928689));
#3831=DIRECTION('',(-1.,0.,0.));
#3832=DIRECTION('',(1.,0.,0.));
#3833=DIRECTION('center_axis',(-1.,0.,0.));
#3834=DIRECTION('ref_axis',(0.,0.876306680043864,0.481753674101715));
#3835=DIRECTION('',(-1.,0.,0.));
#3836=DIRECTION('',(1.,0.,0.));
#3837=DIRECTION('center_axis',(-1.,0.,0.));
#3838=DIRECTION('ref_axis',(0.,0.968583161128631,0.248689887164855));
#3839=DIRECTION('',(-1.,0.,0.));
#3840=DIRECTION('',(1.,0.,0.));
#3841=DIRECTION('center_axis',(-1.,0.,0.));
#3842=DIRECTION('ref_axis',(0.,0.,-1.));
#3843=DIRECTION('center_axis',(1.,0.,0.));
#3844=DIRECTION('ref_axis',(0.,0.,-1.));
#3845=DIRECTION('',(-0.707106781186546,-8.65956056235495E-17,0.707106781186549));
#3846=DIRECTION('center_axis',(1.,0.,0.));
#3847=DIRECTION('ref_axis',(0.,0.,-1.));
#3848=DIRECTION('center_axis',(1.,0.,0.));
#3849=DIRECTION('ref_axis',(0.,0.,-1.));
#3850=DIRECTION('center_axis',(1.,0.,0.));
#3851=DIRECTION('ref_axis',(0.,0.,-1.));
#3852=DIRECTION('center_axis',(1.,0.,0.));
#3853=DIRECTION('ref_axis',(0.,0.,-1.));
#3854=DIRECTION('center_axis',(1.,0.,0.));
#3855=DIRECTION('ref_axis',(0.,0.,-1.));
#3856=DIRECTION('center_axis',(1.,0.,0.));
#3857=DIRECTION('ref_axis',(0.,0.,-1.));
#3858=DIRECTION('center_axis',(1.,0.,0.));
#3859=DIRECTION('ref_axis',(0.,0.,-1.));
#3860=DIRECTION('center_axis',(1.,0.,0.));
#3861=DIRECTION('ref_axis',(0.,0.,-1.));
#3862=DIRECTION('center_axis',(1.,0.,0.));
#3863=DIRECTION('ref_axis',(0.,0.,-1.));
#3864=DIRECTION('center_axis',(1.,0.,0.));
#3865=DIRECTION('ref_axis',(0.,0.,-1.));
#3866=DIRECTION('center_axis',(1.,0.,0.));
#3867=DIRECTION('ref_axis',(0.,0.,-1.));
#3868=DIRECTION('center_axis',(1.,0.,0.));
#3869=DIRECTION('ref_axis',(0.,0.,-1.));
#3870=DIRECTION('center_axis',(1.,0.,0.));
#3871=DIRECTION('ref_axis',(0.,0.,-1.));
#3872=DIRECTION('center_axis',(1.,0.,0.));
#3873=DIRECTION('ref_axis',(0.,0.,-1.));
#3874=DIRECTION('center_axis',(1.,0.,0.));
#3875=DIRECTION('ref_axis',(0.,0.,-1.));
#3876=DIRECTION('center_axis',(1.,0.,0.));
#3877=DIRECTION('ref_axis',(0.,0.,-1.));
#3878=DIRECTION('center_axis',(1.,0.,0.));
#3879=DIRECTION('ref_axis',(0.,0.,-1.));
#3880=DIRECTION('center_axis',(1.,0.,0.));
#3881=DIRECTION('ref_axis',(0.,0.,-1.));
#3882=DIRECTION('center_axis',(1.,0.,0.));
#3883=DIRECTION('ref_axis',(0.,0.,-1.));
#3884=DIRECTION('center_axis',(1.,0.,0.));
#3885=DIRECTION('ref_axis',(0.,0.,-1.));
#3886=DIRECTION('center_axis',(1.,0.,0.));
#3887=DIRECTION('ref_axis',(0.,0.,-1.));
#3888=DIRECTION('center_axis',(1.,0.,0.));
#3889=DIRECTION('ref_axis',(0.,0.,-1.));
#3890=DIRECTION('center_axis',(1.,0.,0.));
#3891=DIRECTION('ref_axis',(0.,0.,-1.));
#3892=DIRECTION('center_axis',(1.,0.,0.));
#3893=DIRECTION('ref_axis',(0.,0.,-1.));
#3894=DIRECTION('center_axis',(1.,0.,0.));
#3895=DIRECTION('ref_axis',(0.,0.,-1.));
#3896=DIRECTION('center_axis',(1.,0.,0.));
#3897=DIRECTION('ref_axis',(0.,0.,-1.));
#3898=DIRECTION('center_axis',(1.,0.,0.));
#3899=DIRECTION('ref_axis',(0.,0.,-1.));
#3900=DIRECTION('',(1.,0.,0.));
#3901=DIRECTION('center_axis',(1.,0.,0.));
#3902=DIRECTION('ref_axis',(0.,0.,-1.));
#3903=DIRECTION('',(-1.,0.,0.));
#3904=DIRECTION('center_axis',(1.,0.,0.));
#3905=DIRECTION('ref_axis',(0.,0.,-1.));
#3906=DIRECTION('center_axis',(1.,0.,0.));
#3907=DIRECTION('ref_axis',(0.,0.,-1.));
#3908=DIRECTION('center_axis',(1.,0.,0.));
#3909=DIRECTION('ref_axis',(0.,0.,-1.));
#3910=DIRECTION('center_axis',(1.,0.,0.));
#3911=DIRECTION('ref_axis',(0.,0.,-1.));
#3912=DIRECTION('center_axis',(1.,0.,0.));
#3913=DIRECTION('ref_axis',(0.,0.,-1.));
#3914=DIRECTION('center_axis',(1.,0.,0.));
#3915=DIRECTION('ref_axis',(0.,0.,-1.));
#3916=DIRECTION('center_axis',(1.,0.,0.));
#3917=DIRECTION('ref_axis',(0.,0.,-1.));
#3918=DIRECTION('center_axis',(1.,0.,0.));
#3919=DIRECTION('ref_axis',(0.,0.,-1.));
#3920=DIRECTION('center_axis',(1.,0.,0.));
#3921=DIRECTION('ref_axis',(0.,0.,-1.));
#3922=DIRECTION('center_axis',(1.,0.,0.));
#3923=DIRECTION('ref_axis',(0.,0.,-1.));
#3924=DIRECTION('center_axis',(1.,0.,0.));
#3925=DIRECTION('ref_axis',(0.,0.,-1.));
#3926=DIRECTION('center_axis',(1.,0.,0.));
#3927=DIRECTION('ref_axis',(0.,0.,-1.));
#3928=DIRECTION('center_axis',(1.,0.,0.));
#3929=DIRECTION('ref_axis',(0.,0.,-1.));
#3930=DIRECTION('center_axis',(1.,0.,0.));
#3931=DIRECTION('ref_axis',(0.,0.,-1.));
#3932=DIRECTION('center_axis',(1.,0.,0.));
#3933=DIRECTION('ref_axis',(0.,0.,-1.));
#3934=DIRECTION('center_axis',(1.,0.,0.));
#3935=DIRECTION('ref_axis',(0.,0.,-1.));
#3936=DIRECTION('center_axis',(1.,0.,0.));
#3937=DIRECTION('ref_axis',(0.,0.,-1.));
#3938=DIRECTION('center_axis',(1.,0.,0.));
#3939=DIRECTION('ref_axis',(0.,0.,-1.));
#3940=DIRECTION('center_axis',(1.,0.,0.));
#3941=DIRECTION('ref_axis',(0.,0.,-1.));
#3942=DIRECTION('center_axis',(1.,0.,0.));
#3943=DIRECTION('ref_axis',(0.,0.,-1.));
#3944=DIRECTION('center_axis',(1.,0.,0.));
#3945=DIRECTION('ref_axis',(0.,0.,-1.));
#3946=DIRECTION('center_axis',(1.,0.,0.));
#3947=DIRECTION('ref_axis',(0.,0.,-1.));
#3948=DIRECTION('center_axis',(1.,0.,0.));
#3949=DIRECTION('ref_axis',(0.,0.,-1.));
#3950=DIRECTION('center_axis',(1.,0.,0.));
#3951=DIRECTION('ref_axis',(0.,0.,-1.));
#3952=DIRECTION('center_axis',(1.,0.,0.));
#3953=DIRECTION('ref_axis',(0.,0.,-1.));
#3954=DIRECTION('center_axis',(1.,0.,0.));
#3955=DIRECTION('ref_axis',(0.,0.,-1.));
#3956=DIRECTION('center_axis',(1.,0.,0.));
#3957=DIRECTION('ref_axis',(0.,0.,-1.));
#3958=DIRECTION('center_axis',(1.,0.,0.));
#3959=DIRECTION('ref_axis',(0.,0.,-1.));
#3960=DIRECTION('center_axis',(1.,0.,0.));
#3961=DIRECTION('ref_axis',(0.,0.,-1.));
#3962=DIRECTION('center_axis',(1.,0.,0.));
#3963=DIRECTION('ref_axis',(0.,0.,-1.));
#3964=DIRECTION('center_axis',(1.,0.,0.));
#3965=DIRECTION('ref_axis',(0.,0.,-1.));
#3966=DIRECTION('center_axis',(1.,0.,0.));
#3967=DIRECTION('ref_axis',(0.,0.,-1.));
#3968=DIRECTION('center_axis',(1.,0.,0.));
#3969=DIRECTION('ref_axis',(0.,0.,-1.));
#3970=DIRECTION('center_axis',(1.,0.,0.));
#3971=DIRECTION('ref_axis',(0.,0.,-1.));
#3972=DIRECTION('center_axis',(1.,0.,0.));
#3973=DIRECTION('ref_axis',(0.,0.,-1.));
#3974=DIRECTION('center_axis',(1.,0.,0.));
#3975=DIRECTION('ref_axis',(0.,0.,-1.));
#3976=DIRECTION('center_axis',(1.,0.,0.));
#3977=DIRECTION('ref_axis',(0.,0.,-1.));
#3978=DIRECTION('center_axis',(1.,0.,0.));
#3979=DIRECTION('ref_axis',(0.,0.,-1.));
#3980=DIRECTION('center_axis',(1.,0.,0.));
#3981=DIRECTION('ref_axis',(0.,0.,-1.));
#3982=DIRECTION('center_axis',(1.,0.,0.));
#3983=DIRECTION('ref_axis',(0.,0.,-1.));
#3984=DIRECTION('center_axis',(1.,0.,0.));
#3985=DIRECTION('ref_axis',(0.,0.,-1.));
#3986=DIRECTION('center_axis',(1.,0.,0.));
#3987=DIRECTION('ref_axis',(0.,0.,-1.));
#3988=DIRECTION('center_axis',(1.,0.,0.));
#3989=DIRECTION('ref_axis',(0.,0.,-1.));
#3990=DIRECTION('center_axis',(1.,0.,0.));
#3991=DIRECTION('ref_axis',(0.,0.,-1.));
#3992=DIRECTION('center_axis',(1.,0.,0.));
#3993=DIRECTION('ref_axis',(0.,0.,-1.));
#3994=DIRECTION('center_axis',(-1.,0.,0.));
#3995=DIRECTION('ref_axis',(0.,1.,0.));
#3996=DIRECTION('center_axis',(1.,0.,0.));
#3997=DIRECTION('ref_axis',(0.,0.,-1.));
#3998=DIRECTION('center_axis',(1.,0.,0.));
#3999=DIRECTION('ref_axis',(0.,0.,-1.));
#4000=DIRECTION('',(-0.702378778976759,8.71707730133816E-17,-0.7118033793423));
#4001=DIRECTION('center_axis',(1.,0.,0.));
#4002=DIRECTION('ref_axis',(0.,0.,-1.));
#4003=DIRECTION('center_axis',(1.,0.,0.));
#4004=DIRECTION('ref_axis',(0.,0.,-1.));
#4005=DIRECTION('center_axis',(-1.,0.,0.));
#4006=DIRECTION('ref_axis',(0.,0.,1.));
#4007=DIRECTION('center_axis',(1.,0.,0.));
#4008=DIRECTION('ref_axis',(0.,0.,-1.));
#4009=DIRECTION('center_axis',(1.,0.,0.));
#4010=DIRECTION('ref_axis',(0.,0.,-1.));
#4011=DIRECTION('',(-1.,0.,0.));
#4663=CARTESIAN_POINT('',(0.,0.,0.));
#4664=CARTESIAN_POINT('Origin',(50.5120935137584,0.,0.));
#4665=CARTESIAN_POINT('',(50.5120935137584,-1.28658893794659E-15,10.5057959473896));
#4666=CARTESIAN_POINT('Origin',(50.5120935137584,0.,0.));
#4667=CARTESIAN_POINT('',(50.0120935137584,-1.22535659798922E-15,10.0057959473896));
#4668=CARTESIAN_POINT('Origin',(50.5120935137584,-1.22535659798922E-15,
10.0057959473896));
#4669=CARTESIAN_POINT('Origin',(50.0120935137584,0.,0.));
#4670=CARTESIAN_POINT('Origin',(50.0120935137584,0.,-10.5057959473896));
#4671=CARTESIAN_POINT('',(50.0120935137584,-1.16412425803185E-15,9.50579594738959));
#4672=CARTESIAN_POINT('Origin',(50.0120935137584,0.,0.));
#4673=CARTESIAN_POINT('Origin',(54.0077062393936,0.,0.));
#4674=CARTESIAN_POINT('',(58.0033189650289,-1.28658893794659E-15,10.5057959473896));
#4675=CARTESIAN_POINT('Origin',(58.0033189650289,0.,0.));
#4676=CARTESIAN_POINT('',(54.0077062393936,-1.28658893794659E-15,10.5057959473896));
#4677=CARTESIAN_POINT('Origin',(65.0333054217745,2.89627205572787,11.2802348949791));
#4678=CARTESIAN_POINT('',(58.5152881956451,1.99731386475336,10.8422004546896));
#4679=CARTESIAN_POINT('',(58.5152881956451,3.47301042256638,10.4633059774983));
#4680=CARTESIAN_POINT('Ctrl Pts',(58.5152881956451,1.99731386475335,10.8422004546895));
#4681=CARTESIAN_POINT('Ctrl Pts',(58.4654152249681,2.02482541039242,10.7857397588542));
#4682=CARTESIAN_POINT('Ctrl Pts',(58.4186772780868,2.05797507265433,10.7312801542195));
#4683=CARTESIAN_POINT('Ctrl Pts',(58.3120945049187,2.15482072622166,10.6021965229197));
#4684=CARTESIAN_POINT('Ctrl Pts',(58.2507030237862,2.23349798161002,10.5226028552003));
#4685=CARTESIAN_POINT('Ctrl Pts',(58.1653214105115,2.42316764831179,10.3917259702023));
#4686=CARTESIAN_POINT('Ctrl Pts',(58.1417842183134,2.5345267480614,10.3406794321384));
#4687=CARTESIAN_POINT('Ctrl Pts',(58.1417842183134,2.76063758906463,10.2826240355627));
#4688=CARTESIAN_POINT('Ctrl Pts',(58.1653214105115,2.88281416932137,10.2737088024122));
#4689=CARTESIAN_POINT('Ctrl Pts',(58.2507030237862,3.11207338545657,10.2970230322));
#4690=CARTESIAN_POINT('Ctrl Pts',(58.3120945049187,3.21936333178,10.3288684380602));
#4691=CARTESIAN_POINT('Ctrl Pts',(58.4186772780868,3.36641633857932,10.3953295370257));
#4692=CARTESIAN_POINT('Ctrl Pts',(58.4654152249681,3.4217017236835,10.4270828807697));
#4693=CARTESIAN_POINT('Ctrl Pts',(58.5152881956451,3.47301042256638,10.4633059774983));
#4694=CARTESIAN_POINT('',(64.5333054217746,1.99731386475336,10.8422004546896));
#4695=CARTESIAN_POINT('',(65.0333054217745,1.99731386475335,10.8422004546896));
#4696=CARTESIAN_POINT('',(64.5333054217746,3.47301042256638,10.4633059774983));
#4697=CARTESIAN_POINT('Ctrl Pts',(64.5333054217746,3.47301042256638,10.4633059774983));
#4698=CARTESIAN_POINT('Ctrl Pts',(64.5841440169343,3.42140080495871,10.4268704371039));
#4699=CARTESIAN_POINT('Ctrl Pts',(64.6317941862906,3.36574304661788,10.3949381862959));
#4700=CARTESIAN_POINT('Ctrl Pts',(64.7397191574786,3.21851020835991,10.328616066089));
#4701=CARTESIAN_POINT('Ctrl Pts',(64.8016959801978,3.11150967133897,10.2969249363867));
#4702=CARTESIAN_POINT('Ctrl Pts',(64.8879780992218,2.88267500902188,10.2737355458811));
#4703=CARTESIAN_POINT('Ctrl Pts',(64.911821119031,2.76062757856656,10.2826266058217));
#4704=CARTESIAN_POINT('Ctrl Pts',(64.911821119031,2.53453675855947,10.3406768618793));
#4705=CARTESIAN_POINT('Ctrl Pts',(64.8879780992218,2.42330247917621,10.3916823646972));
#4706=CARTESIAN_POINT('Ctrl Pts',(64.8016959801978,2.23394471003842,10.5222453218365));
#4707=CARTESIAN_POINT('Ctrl Pts',(64.7397191574786,2.15544674284921,10.6015643723334));
#4708=CARTESIAN_POINT('Ctrl Pts',(64.6317941862906,2.05837654824586,10.7306128500846));
#4709=CARTESIAN_POINT('Ctrl Pts',(64.5841440169343,2.0249867619646,10.7854086243495));
#4710=CARTESIAN_POINT('Ctrl Pts',(64.5333054217746,1.99731386475335,10.8422004546895));
#4711=CARTESIAN_POINT('',(65.0333054217745,3.47301042256639,10.4633059774983));
#4712=CARTESIAN_POINT('Origin',(65.0333054217745,5.61056068645085,10.2055720021147));
#4713=CARTESIAN_POINT('',(58.5152881956451,4.63091018458434,10.0048610303352));
#4714=CARTESIAN_POINT('',(58.5152881956451,5.96601779663743,9.270879409431));
#4715=CARTESIAN_POINT('Ctrl Pts',(58.5152881956451,4.63091018458433,10.0048610303352));
#4716=CARTESIAN_POINT('Ctrl Pts',(58.4654152249681,4.64351620035041,9.94333230790271));
#4717=CARTESIAN_POINT('Ctrl Pts',(58.4186772780868,4.66208085208276,9.88233966612439));
#4718=CARTESIAN_POINT('Ctrl Pts',(58.3120945049187,4.72378212765379,9.73322689981203));
#4719=CARTESIAN_POINT('Ctrl Pts',(58.2507030237862,4.78019345214259,9.63656757576151));
#4720=CARTESIAN_POINT('Ctrl Pts',(58.1653214105115,4.93135653972417,9.46263350076087));
#4721=CARTESIAN_POINT('Ctrl Pts',(58.1417842183134,5.02652233078881,9.38549680160669));
#4722=CARTESIAN_POINT('Ctrl Pts',(58.1417842183134,5.23109169390945,9.273033842535));
#4723=CARTESIAN_POINT('Ctrl Pts',(58.1653214105115,5.34721274390418,9.23401461786969));
#4724=CARTESIAN_POINT('Ctrl Pts',(58.2507030237862,5.57506737336155,9.19958193966468));
#4725=CARTESIAN_POINT('Ctrl Pts',(58.3120945049187,5.6869062391189,9.20374493889506));
#4726=CARTESIAN_POINT('Ctrl Pts',(58.4186772780868,5.84586750850063,9.23154744455494));
#4727=CARTESIAN_POINT('Ctrl Pts',(58.4654152249681,5.90731273704185,9.24855428243148));
#4728=CARTESIAN_POINT('Ctrl Pts',(58.5152881956451,5.96601779663743,9.270879409431));
#4729=CARTESIAN_POINT('',(64.5333054217746,4.63091018458434,10.0048610303352));
#4730=CARTESIAN_POINT('',(65.0333054217746,4.63091018458433,10.0048610303352));
#4731=CARTESIAN_POINT('',(64.5333054217746,5.96601779663743,9.270879409431));
#4732=CARTESIAN_POINT('Ctrl Pts',(64.5333054217746,5.96601779663743,9.270879409431));
#4733=CARTESIAN_POINT('Ctrl Pts',(64.5841440169343,5.90696843964088,9.24842334851786));
#4734=CARTESIAN_POINT('Ctrl Pts',(64.6317941862906,5.84511804427544,9.23133582972996));
#4735=CARTESIAN_POINT('Ctrl Pts',(64.7397191574786,5.68601715578279,9.20371265882047));
#4736=CARTESIAN_POINT('Ctrl Pts',(64.8016959801978,5.5744969739228,9.19962711571201));
#4737=CARTESIAN_POINT('Ctrl Pts',(64.8879780992218,5.34708460641165,9.23407512890248));
#4738=CARTESIAN_POINT('Ctrl Pts',(64.9118211190309,5.23108263710702,9.27303882155427));
#4739=CARTESIAN_POINT('Ctrl Pts',(64.9118211190309,5.02653138759124,9.38549182258742));
#4740=CARTESIAN_POINT('Ctrl Pts',(64.8879780992218,4.9314762903809,9.46255773413038));
#4741=CARTESIAN_POINT('Ctrl Pts',(64.8016959801978,4.78053723084404,9.63611017812334));
#4742=CARTESIAN_POINT('Ctrl Pts',(64.7397191574786,4.72423126735984,9.73245892539434));
#4743=CARTESIAN_POINT('Ctrl Pts',(64.6317941862906,4.66230376279031,9.88159348365645));
#4744=CARTESIAN_POINT('Ctrl Pts',(64.5841440169343,4.64359013296362,9.9429714500931));
#4745=CARTESIAN_POINT('Ctrl Pts',(64.5333054217746,4.63091018458433,10.0048610303352));
#4746=CARTESIAN_POINT('',(65.0333054217746,5.96601779663744,9.270879409431));
#4747=CARTESIAN_POINT('Origin',(65.0333054217745,7.97231715504529,8.48965548688909));
#4748=CARTESIAN_POINT('',(58.5152881956451,6.97352938622157,8.53887939213984));
#4749=CARTESIAN_POINT('',(58.5152881956451,8.08415833106712,7.49592939215974));
#4750=CARTESIAN_POINT('Ctrl Pts',(58.5152881956451,6.97352938622157,8.53887939213984));
#4751=CARTESIAN_POINT('Ctrl Pts',(58.4654152249681,6.97043778978238,8.47614871902753));
#4752=CARTESIAN_POINT('Ctrl Pts',(58.4186772780868,6.97325094564081,8.41245543210374));
#4753=CARTESIAN_POINT('Ctrl Pts',(58.3120945049187,6.99593092515002,8.25268283428458));
#4754=CARTESIAN_POINT('Ctrl Pts',(58.2507030237862,7.02653178775528,8.14503131472124));
#4755=CARTESIAN_POINT('Ctrl Pts',(58.1653214105115,7.12969016348498,7.93896896733498));
#4756=CARTESIAN_POINT('Ctrl Pts',(58.1417842183134,7.20268302921674,7.84058888958738));
#4757=CARTESIAN_POINT('Ctrl Pts',(58.1417842183134,7.37285706901645,7.68078482934798));
#4758=CARTESIAN_POINT('Ctrl Pts',(58.1653214105115,7.47562627611464,7.61411333455621));
#4759=CARTESIAN_POINT('Ctrl Pts',(58.2507030237862,7.68775937453466,7.52409728016453));
#4760=CARTESIAN_POINT('Ctrl Pts',(58.3120945049187,7.79711991247583,7.50031629621303));
#4761=CARTESIAN_POINT('Ctrl Pts',(58.4186772780868,7.95800132326607,7.48771327488625));
#4762=CARTESIAN_POINT('Ctrl Pts',(58.4654152249681,8.02174556555534,7.48890500472477));
#4763=CARTESIAN_POINT('Ctrl Pts',(58.5152881956451,8.08415833106712,7.49592939215974));
#4764=CARTESIAN_POINT('',(64.5333054217746,6.97352938622157,8.53887939213984));
#4765=CARTESIAN_POINT('',(65.0333054217745,6.97352938622157,8.53887939213985));
#4766=CARTESIAN_POINT('',(64.5333054217746,8.08415833106712,7.49592939215974));
#4767=CARTESIAN_POINT('Ctrl Pts',(64.5333054217746,8.08415833106712,7.49592939215974));
#4768=CARTESIAN_POINT('Ctrl Pts',(64.5841440169343,8.02137952295014,7.48886380762262));
#4769=CARTESIAN_POINT('Ctrl Pts',(64.6317941862906,7.95722277837072,7.48769469250372));
#4770=CARTESIAN_POINT('Ctrl Pts',(64.7397191574786,7.79625073359952,7.50050613631088));
#4771=CARTESIAN_POINT('Ctrl Pts',(64.8016959801978,7.68721813006929,7.52428288949533));
#4772=CARTESIAN_POINT('Ctrl Pts',(64.8879780992218,7.47551721277898,7.61420381102219));
#4773=CARTESIAN_POINT('Ctrl Pts',(64.9118211190309,7.37284953498186,7.68079190427738));
#4774=CARTESIAN_POINT('Ctrl Pts',(64.9118211190309,7.20269056325133,7.84058181465798));
#4775=CARTESIAN_POINT('Ctrl Pts',(64.8879780992218,7.12978730955983,7.93886580027521));
#4776=CARTESIAN_POINT('Ctrl Pts',(64.8016959801978,7.02675101584962,8.1445027927845));
#4777=CARTESIAN_POINT('Ctrl Pts',(64.7397191574786,6.99617496683501,8.25182729069262));
#4778=CARTESIAN_POINT('Ctrl Pts',(64.6317941862906,6.97328128516483,8.41167725669145));
#4779=CARTESIAN_POINT('Ctrl Pts',(64.5841440169343,6.97041965797865,8.47578081193636));
#4780=CARTESIAN_POINT('Ctrl Pts',(64.5333054217746,6.97352938622157,8.53887939213984));
#4781=CARTESIAN_POINT('',(65.0333054217745,8.08415833106713,7.49592939215974));
#4782=CARTESIAN_POINT('Origin',(65.0333054217745,9.83314361665672,6.24030269465341));
#4783=CARTESIAN_POINT('',(58.5152881956451,8.87797608967546,6.53636855793469));
#4784=CARTESIAN_POINT('',(58.5152881956451,9.69434146610128,5.2499825630792));
#4785=CARTESIAN_POINT('Ctrl Pts',(58.5152881956451,8.87797608967545,6.53636855793469));
#4786=CARTESIAN_POINT('Ctrl Pts',(58.4654152249681,8.85938113740538,6.47637753304147));
#4787=CARTESIAN_POINT('Ctrl Pts',(58.4186772780868,8.84626603646124,6.41398568443713));
#4788=CARTESIAN_POINT('Ctrl Pts',(58.3120945049187,8.82849965338492,6.25359235503467));
#4789=CARTESIAN_POINT('Ctrl Pts',(58.2507030237862,8.83136728936705,6.14171278084726));
#4790=CARTESIAN_POINT('Ctrl Pts',(58.1653214105115,8.88003913310781,5.91646981620596));
#4791=CARTESIAN_POINT('Ctrl Pts',(58.1417842183134,8.9262726633038,5.80302794196644));
#4792=CARTESIAN_POINT('Ctrl Pts',(58.1417842183134,9.0513587190056,5.6059238573824));
#4793=CARTESIAN_POINT('Ctrl Pts',(58.1653214105115,9.13431871596657,5.51578930768254));
#4794=CARTESIAN_POINT('Ctrl Pts',(58.2507030237862,9.31740118060456,5.37584591685752));
#4795=CARTESIAN_POINT('Ctrl Pts',(58.3120945049187,9.41741186593077,5.32561519640614));
#4796=CARTESIAN_POINT('Ctrl Pts',(58.4186772780868,9.57010464740912,5.27339854227333));
#4797=CARTESIAN_POINT('Ctrl Pts',(58.4654152249681,9.63214261826849,5.25870028330521));
#4798=CARTESIAN_POINT('Ctrl Pts',(58.5152881956451,9.69434146610128,5.24998256307919));
#4799=CARTESIAN_POINT('',(64.5333054217746,8.87797608967546,6.53636855793469));
#4800=CARTESIAN_POINT('',(65.0333054217745,8.87797608967545,6.5363685579347));
#4801=CARTESIAN_POINT('',(64.5333054217746,9.69434146610128,5.2499825630792));
#4802=CARTESIAN_POINT('Ctrl Pts',(64.5333054217746,9.69434146610128,5.24998256307919));
#4803=CARTESIAN_POINT('Ctrl Pts',(64.5841440169343,9.63177783026215,5.25875141157996));
#4804=CARTESIAN_POINT('Ctrl Pts',(64.6317941862906,9.5693459406827,5.2735741599327));
#4805=CARTESIAN_POINT('Ctrl Pts',(64.7397191574786,9.41661720521969,5.3260152283249));
#4806=CARTESIAN_POINT('Ctrl Pts',(64.8016959801978,9.31692309949288,5.37616029695489));
#4807=CARTESIAN_POINT('Ctrl Pts',(64.8879780992218,9.13423557963827,5.51590406461261));
#4808=CARTESIAN_POINT('Ctrl Pts',(64.9118211190309,9.05135318112996,5.60593258367809));
#4809=CARTESIAN_POINT('Ctrl Pts',(64.9118211190309,8.92627820117944,5.80301921567074));
#4810=CARTESIAN_POINT('Ctrl Pts',(64.8879780992218,8.88010757055562,5.91634573108269));
#4811=CARTESIAN_POINT('Ctrl Pts',(64.8016959801978,8.83144819194687,6.14114634358899));
#4812=CARTESIAN_POINT('Ctrl Pts',(64.7397191574786,8.82852326301226,6.25270299921878));
#4813=CARTESIAN_POINT('Ctrl Pts',(64.6317941862906,8.84610189845785,6.41322441170358));
#4814=CARTESIAN_POINT('Ctrl Pts',(64.5841440169343,8.8592720804726,6.47602569362431));
#4815=CARTESIAN_POINT('Ctrl Pts',(64.5333054217746,8.87797608967545,6.53636855793469));
#4816=CARTESIAN_POINT('',(65.0333054217745,9.69434146610128,5.24998256307919));
#4817=CARTESIAN_POINT('Origin',(65.0333054217745,11.0761175010611,3.59884873388474));
#4818=CARTESIAN_POINT('',(58.5152881956451,10.2245869045029,4.1231536481525));
#4819=CARTESIAN_POINT('',(58.5152881956451,10.6953934735264,2.67416002147514));
#4820=CARTESIAN_POINT('Ctrl Pts',(58.5152881956451,10.2245869045029,4.12315364815251));
#4821=CARTESIAN_POINT('Ctrl Pts',(58.4654152249681,10.1916569856405,4.06967172820395));
#4822=CARTESIAN_POINT('Ctrl Pts',(58.4186772780868,10.1634376979201,4.01250162722806));
#4823=CARTESIAN_POINT('Ctrl Pts',(58.3120945049187,10.1063412794472,3.86156566901406));
#4824=CARTESIAN_POINT('Ctrl Pts',(58.2507030237862,10.081295504691,3.75248784531307));
#4825=CARTESIAN_POINT('Ctrl Pts',(58.1653214105115,10.072422585498,3.52221710727082));
#4826=CARTESIAN_POINT('Ctrl Pts',(58.1417842183134,10.088991757421,3.40084140670787));
#4827=CARTESIAN_POINT('Ctrl Pts',(58.1417842183134,10.1611302121108,3.17882207231172));
#4828=CARTESIAN_POINT('Ctrl Pts',(58.1653214105115,10.21906831722,3.07088795295311));
#4829=CARTESIAN_POINT('Ctrl Pts',(58.2507030237862,10.3615964034925,2.88981038361606));
#4830=CARTESIAN_POINT('Ctrl Pts',(58.3120945049187,10.4459731970312,2.81628610756644));
#4831=CARTESIAN_POINT('Ctrl Pts',(58.4186772780868,10.5808831001726,2.72773678504619));
#4832=CARTESIAN_POINT('Ctrl Pts',(58.4654152249681,10.6373167257333,2.69807208293881));
#4833=CARTESIAN_POINT('Ctrl Pts',(58.5152881956451,10.6953934735264,2.67416002147513));
#4834=CARTESIAN_POINT('',(64.5333054217746,10.2245869045029,4.1231536481525));
#4835=CARTESIAN_POINT('',(65.0333054217745,10.2245869045029,4.12315364815251));
#4836=CARTESIAN_POINT('',(64.5333054217746,10.6953934735264,2.67416002147514));
#4837=CARTESIAN_POINT('Ctrl Pts',(64.5333054217746,10.6953934735264,2.67416002147513));
#4838=CARTESIAN_POINT('Ctrl Pts',(64.5841440169343,10.6369761132978,2.69821232401292));
#4839=CARTESIAN_POINT('Ctrl Pts',(64.6317941862906,10.580191903949,2.72809556804403));
#4840=CARTESIAN_POINT('Ctrl Pts',(64.7397191574786,10.4453029859404,2.81687119582944));
#4841=CARTESIAN_POINT('Ctrl Pts',(64.8016959801978,10.3612115253291,2.89023378082229));
#4842=CARTESIAN_POINT('Ctrl Pts',(64.8879780992218,10.2190163316603,3.07101977974729));
#4843=CARTESIAN_POINT('Ctrl Pts',(64.9118211190309,10.1611270183592,3.17883190166845));
#4844=CARTESIAN_POINT('Ctrl Pts',(64.9118211190309,10.0889949511726,3.40083157735114));
#4845=CARTESIAN_POINT('Ctrl Pts',(64.8879780992218,10.0724580141423,3.5220799008087));
#4846=CARTESIAN_POINT('Ctrl Pts',(64.8016959801978,10.0812329983496,3.75191908406943));
#4847=CARTESIAN_POINT('Ctrl Pts',(64.7397191574786,10.1061429735371,3.86069838247098));
#4848=CARTESIAN_POINT('Ctrl Pts',(64.6317941862906,10.1630893957837,4.01180509073886));
#4849=CARTESIAN_POINT('Ctrl Pts',(64.5841440169343,10.1914638560269,4.06935806382539));
#4850=CARTESIAN_POINT('Ctrl Pts',(64.5333054217746,10.2245869045029,4.1231536481525));
#4851=CARTESIAN_POINT('',(65.0333054217745,10.6953934735264,2.67416002147513));
#4852=CARTESIAN_POINT('Origin',(65.0333054217745,11.6231381877631,0.731265871526308));
#4853=CARTESIAN_POINT('',(58.5152881956451,10.9287493207203,1.45086583075851));
#4854=CARTESIAN_POINT('',(58.5152881956451,11.0244145741041,-0.0696898291507925));
#4855=CARTESIAN_POINT('Ctrl Pts',(58.5152881956451,10.9287493207203,1.45086583075852));
#4856=CARTESIAN_POINT('Ctrl Pts',(58.4654152249681,10.8835535431755,1.40725348147776));
#4857=CARTESIAN_POINT('Ctrl Pts',(58.4186772780868,10.8420031903095,1.35889733583154));
#4858=CARTESIAN_POINT('Ctrl Pts',(58.3120945049187,10.7491643143985,1.22690261016421));
#4859=CARTESIAN_POINT('Ctrl Pts',(58.2507030237862,10.6977788470438,1.12748029777294));
#4860=CARTESIAN_POINT('Ctrl Pts',(58.1653214105115,10.6319186830624,0.906650543677475));
#4861=CARTESIAN_POINT('Ctrl Pts',(58.1417842183134,10.6177823947033,0.784967498446075));
#4862=CARTESIAN_POINT('Ctrl Pts',(58.1417842183134,10.6324405239663,0.551983205547912));
#4863=CARTESIAN_POINT('Ctrl Pts',(58.1653214105115,10.6617162729982,0.433031414203771));
#4864=CARTESIAN_POINT('Ctrl Pts',(58.2507030237862,10.7547344170632,0.222197435992864));
#4865=CARTESIAN_POINT('Ctrl Pts',(58.3120945049187,10.8181756145601,0.129999405012576));
#4866=CARTESIAN_POINT('Ctrl Pts',(58.4186772780868,10.9268257539862,0.0106812937004497));
#4867=CARTESIAN_POINT('Ctrl Pts',(58.4654152249681,10.9741091020059,-0.0320859092136418));
#4868=CARTESIAN_POINT('Ctrl Pts',(58.5152881956451,11.0244145741041,-0.069689829150799));
#4869=CARTESIAN_POINT('',(64.5333054217746,10.9287493207203,1.45086583075851));
#4870=CARTESIAN_POINT('',(65.0333054217745,10.9287493207203,1.45086583075852));
#4871=CARTESIAN_POINT('',(64.5333054217746,11.0244145741041,-0.0696898291507925));
#4872=CARTESIAN_POINT('Ctrl Pts',(64.5333054217746,11.0244145741041,-0.0696898291507991));
#4873=CARTESIAN_POINT('Ctrl Pts',(64.5841440169343,10.9738140670733,-0.0318653672026165));
#4874=CARTESIAN_POINT('Ctrl Pts',(64.6317941862906,10.9262454986663,0.0112006983815072));
#4875=CARTESIAN_POINT('Ctrl Pts',(64.7397191574786,10.8176719649172,0.130732786372444));
#4876=CARTESIAN_POINT('Ctrl Pts',(64.8016959801978,10.7544669251584,0.222703246704341));
#4877=CARTESIAN_POINT('Ctrl Pts',(64.8879780992218,10.6616987046511,0.43317202769978));
#4878=CARTESIAN_POINT('Ctrl Pts',(64.9118211190309,10.6324398750139,0.551993520351058));
#4879=CARTESIAN_POINT('Ctrl Pts',(64.9118211190309,10.6177830436557,0.784957183642929));
#4880=CARTESIAN_POINT('Ctrl Pts',(64.8879780992218,10.6319188767911,0.906508837063128));
#4881=CARTESIAN_POINT('Ctrl Pts',(64.8016959801978,10.6975768592847,1.12694494990463));
#4882=CARTESIAN_POINT('Ctrl Pts',(64.7397191574786,10.7487565532408,1.22611188769709));
#4883=CARTESIAN_POINT('Ctrl Pts',(64.6317941862906,10.8414926091443,1.358309301536));
#4884=CARTESIAN_POINT('Ctrl Pts',(64.5841440169343,10.8832884759249,1.40699770082426));
#4885=CARTESIAN_POINT('Ctrl Pts',(64.5333054217746,10.9287493207203,1.45086583075852));
#4886=CARTESIAN_POINT('',(65.0333054217745,11.0244145741041,-0.0696898291508022));
#4887=CARTESIAN_POINT('Origin',(65.0333054217745,11.4398343552159,-2.18226511494788));
#4888=CARTESIAN_POINT('',(58.5152881956451,10.9462182239883,-1.31258522269331));
#4889=CARTESIAN_POINT('',(58.5152881956451,10.6607311620303,-2.80916081150993));
#4890=CARTESIAN_POINT('Ctrl Pts',(58.5152881956451,10.9462182239883,-1.3125852226933));
#4891=CARTESIAN_POINT('Ctrl Pts',(58.4654152249681,10.8915964046827,-1.34358767700596));
#4892=CARTESIAN_POINT('Ctrl Pts',(58.4186772780868,10.8393257481533,-1.38009147285009));
#4893=CARTESIAN_POINT('Ctrl Pts',(58.3120945049187,10.7165778228152,-1.48485125191443));
#4894=CARTESIAN_POINT('Ctrl Pts',(58.2507030237862,10.6420814007585,-1.56837098345874));
#4895=CARTESIAN_POINT('Ctrl Pts',(58.1653214105115,10.5233722283083,-1.76588420800259));
#4896=CARTESIAN_POINT('Ctrl Pts',(58.1417842183134,10.4794187146543,-1.88022880465161));
#4897=CARTESIAN_POINT('Ctrl Pts',(58.1417842183134,10.4356754943201,-2.1095387960727));
#4898=CARTESIAN_POINT('Ctrl Pts',(58.1653214105115,10.4344493842944,-2.23203408087814));
#4899=CARTESIAN_POINT('Ctrl Pts',(58.2507030237862,10.4721129140633,-2.45937699371878));
#4900=CARTESIAN_POINT('Ctrl Pts',(58.3120945049187,10.5106322717593,-2.56445563826261));
#4901=CARTESIAN_POINT('Ctrl Pts',(58.4186772780868,10.5861957596229,-2.70704534261155));
#4902=CARTESIAN_POINT('Ctrl Pts',(58.4654152249681,10.6213578434494,-2.76022782568649));
#4903=CARTESIAN_POINT('Ctrl Pts',(58.5152881956451,10.6607311620303,-2.80916081150993));
#4904=CARTESIAN_POINT('',(64.5333054217746,10.9462182239883,-1.31258522269331));
#4905=CARTESIAN_POINT('',(65.0333054217745,10.9462182239883,-1.3125852226933));
#4906=CARTESIAN_POINT('',(64.5333054217746,10.6607311620303,-2.80916081150993));
#4907=CARTESIAN_POINT('Ctrl Pts',(64.5333054217746,10.6607311620303,-2.80916081150993));
#4908=CARTESIAN_POINT('Ctrl Pts',(64.5841440169343,10.6211269241497,-2.75994084020421));
#4909=CARTESIAN_POINT('Ctrl Pts',(64.6317941862906,10.5857629047824,-2.70639795235363));
#4910=CARTESIAN_POINT('Ctrl Pts',(64.7397191574786,10.5103268297238,-2.5636200448539));
#4911=CARTESIAN_POINT('Ctrl Pts',(64.8016959801978,10.4719796159174,-2.4588205514493));
#4912=CARTESIAN_POINT('Ctrl Pts',(64.8879780992218,10.4344673370436,-2.2318935159434));
#4913=CARTESIAN_POINT('Ctrl Pts',(64.9118211190309,10.4356774309429,-2.10952864394017));
#4914=CARTESIAN_POINT('Ctrl Pts',(64.9118211190309,10.4794167780314,-1.88023895678415));
#4915=CARTESIAN_POINT('Ctrl Pts',(64.8879780992218,10.5233371749486,-1.76602151082142));
#4916=CARTESIAN_POINT('Ctrl Pts',(64.8016959801978,10.6417526232152,-1.5688392800763));
#4917=CARTESIAN_POINT('Ctrl Pts',(64.7397191574786,10.7159862275429,-1.4855157263049));
#4918=CARTESIAN_POINT('Ctrl Pts',(64.6317941862906,10.8386849696517,-1.38053405659455));
#4919=CARTESIAN_POINT('Ctrl Pts',(64.5841440169343,10.8912760549453,-1.34376950229525));
#4920=CARTESIAN_POINT('Ctrl Pts',(64.5333054217746,10.9462182239883,-1.3125852226933));
#4921=CARTESIAN_POINT('',(65.0333054217745,10.6607311620303,-2.80916081150994));
#4922=CARTESIAN_POINT('Origin',(65.0333054217745,10.5377236573627,-4.95867635844021));
#4923=CARTESIAN_POINT('',(58.5152881956451,10.2758959788686,-3.99356171925254));
#4924=CARTESIAN_POINT('',(58.5152881956451,9.62719480361945,-5.37212188871111));
#4925=CARTESIAN_POINT('Ctrl Pts',(58.5152881956451,10.2758959788686,-3.99356171925253));
#4926=CARTESIAN_POINT('Ctrl Pts',(58.4654152249681,10.2152802075941,-4.01000628037357));
#4927=CARTESIAN_POINT('Ctrl Pts',(58.4186772780868,10.155573604989,-4.03236405867114));
#4928=CARTESIAN_POINT('Ctrl Pts',(58.3120945049187,10.0106293338081,-4.10330644893436));
#4929=CARTESIAN_POINT('Ctrl Pts',(58.2507030237862,9.91770284122587,-4.16567574773471));
#4930=CARTESIAN_POINT('Ctrl Pts',(58.1653214105115,9.75360359419369,-4.32746196042601));
#4931=CARTESIAN_POINT('Ctrl Pts',(58.1417842183134,9.68259461615746,-4.4272834169552));
#4932=CARTESIAN_POINT('Ctrl Pts',(58.1417842183134,9.5831985936359,-4.63851071679507));
#4933=CARTESIAN_POINT('Ctrl Pts',(58.1653214105115,9.55154766555483,-4.75685266581133));
#4934=CARTESIAN_POINT('Ctrl Pts',(58.2507030237862,9.53149004293565,-4.98641972195918));
#4935=CARTESIAN_POINT('Ctrl Pts',(58.3120945049187,9.54266724792246,-5.09777650237764));
#4936=CARTESIAN_POINT('Ctrl Pts',(58.4186772780868,9.58039615237783,-5.2546783642309));
#4937=CARTESIAN_POINT('Ctrl Pts',(58.4654152249681,9.60122760896736,-5.3149344764636));
#4938=CARTESIAN_POINT('Ctrl Pts',(58.5152881956451,9.62719480361944,-5.37212188871111));
#4939=CARTESIAN_POINT('',(64.5333054217746,10.2758959788686,-3.99356171925254));
#4940=CARTESIAN_POINT('',(65.0333054217745,10.2758959788686,-3.99356171925253));
#4941=CARTESIAN_POINT('',(64.5333054217746,9.62719480361945,-5.37212188871111));
#4942=CARTESIAN_POINT('Ctrl Pts',(64.5333054217746,9.62719480361944,-5.37212188871111));
#4943=CARTESIAN_POINT('Ctrl Pts',(64.5841440169343,9.60107531480922,-5.31459907986337));
#4944=CARTESIAN_POINT('Ctrl Pts',(64.6317941862906,9.58013789587829,-5.25394366630695));
#4945=CARTESIAN_POINT('Ctrl Pts',(64.7397191574786,9.54257920554065,-5.09689120032706));
#4946=CARTESIAN_POINT('Ctrl Pts',(64.8016959801978,9.53149931416127,-4.98584761144596));
#4947=CARTESIAN_POINT('Ctrl Pts',(64.8879780992218,9.55160001136319,-4.75672098164969));
#4948=CARTESIAN_POINT('Ctrl Pts',(64.9118211190309,9.58320299414889,-4.63850136522897));
#4949=CARTESIAN_POINT('Ctrl Pts',(64.9118211190309,9.68259021564447,-4.42729276852131));
#4950=CARTESIAN_POINT('Ctrl Pts',(64.8879780992218,9.75353549627729,-4.32758623220826));
#4951=CARTESIAN_POINT('Ctrl Pts',(64.8016959801978,9.91726793220073,-4.16604756830275));
#4952=CARTESIAN_POINT('Ctrl Pts',(64.7397191574786,10.009891076528,-4.10380292387847));
#4953=CARTESIAN_POINT('Ctrl Pts',(64.6317941862906,10.1548428916209,-4.03263338270016));
#4954=CARTESIAN_POINT('Ctrl Pts',(64.5841440169343,10.2149247041221,-4.010102725547));
#4955=CARTESIAN_POINT('Ctrl Pts',(64.5333054217746,10.2758959788686,-3.99356171925253));
#4956=CARTESIAN_POINT('',(65.0333054217745,9.62719480361944,-5.37212188871111));
#4957=CARTESIAN_POINT('Origin',(65.0333054217745,8.9734890270808,-7.42351572959578));
#4958=CARTESIAN_POINT('',(58.5152881956451,8.9599013972947,-6.42360804569852));
#4959=CARTESIAN_POINT('',(58.5152881956451,7.98874638935144,-7.59753279036232));
#4960=CARTESIAN_POINT('Ctrl Pts',(58.5152881956451,8.9599013972947,-6.42360804569851));
#4961=CARTESIAN_POINT('Ctrl Pts',(58.4654152249681,8.89710038588973,-6.42446144137384));
#4962=CARTESIAN_POINT('Ctrl Pts',(58.4186772780868,8.83370942263619,-6.43126838068827));
#4963=CARTESIAN_POINT('Ctrl Pts',(58.3120945049187,8.67567618723855,-6.46393581086227));
#4964=CARTESIAN_POINT('Ctrl Pts',(58.2507030237862,8.57015853741945,-6.50123578449678));
#4965=CARTESIAN_POINT('Ctrl Pts',(58.1653214105115,8.37098017501116,-6.61712936258408));
#4966=CARTESIAN_POINT('Ctrl Pts',(58.1417842183134,8.27737748783543,-6.69615552976207));
#4967=CARTESIAN_POINT('Ctrl Pts',(58.1417842183134,8.12857408077458,-6.87602794993212));
#4968=CARTESIAN_POINT('Ctrl Pts',(58.1653214105115,8.06848707885344,-6.98278070327126));
#4969=CARTESIAN_POINT('Ctrl Pts',(58.2507030237862,7.99196859804205,-7.20014736029998));
#4970=CARTESIAN_POINT('Ctrl Pts',(58.3120945049187,7.97510134542345,-7.31078532053779));
#4971=CARTESIAN_POINT('Ctrl Pts',(58.4186772780868,7.9726250206465,-7.47214061887044));
#4972=CARTESIAN_POINT('Ctrl Pts',(58.4654152249681,7.97781693296876,-7.53568424712284));
#4973=CARTESIAN_POINT('Ctrl Pts',(58.5152881956451,7.98874638935144,-7.59753279036232));
#4974=CARTESIAN_POINT('',(64.5333054217746,8.9599013972947,-6.42360804569852));
#4975=CARTESIAN_POINT('',(65.0333054217745,8.95990139729471,-6.42360804569851));
#4976=CARTESIAN_POINT('',(64.5333054217746,7.98874638935144,-7.59753279036232));
#4977=CARTESIAN_POINT('Ctrl Pts',(64.5333054217746,7.98874638935144,-7.59753279036232));
#4978=CARTESIAN_POINT('Ctrl Pts',(64.5841440169343,7.97775283315432,-7.53532151360656));
#4979=CARTESIAN_POINT('Ctrl Pts',(64.6317941862906,7.97255758969361,-7.47136477705306));
#4980=CARTESIAN_POINT('Ctrl Pts',(64.7397191574786,7.97523623472203,-7.30990593662908));
#4981=CARTESIAN_POINT('Ctrl Pts',(64.8016959801978,7.99211985609405,-7.19959552935062));
#4982=CARTESIAN_POINT('Ctrl Pts',(64.8879780992218,8.06857052864127,-6.98266617408288));
#4983=CARTESIAN_POINT('Ctrl Pts',(64.9118211190309,8.12858066867727,-6.87601998652573));
#4984=CARTESIAN_POINT('Ctrl Pts',(64.9118211190309,8.27737089993274,-6.69616349316845));
#4985=CARTESIAN_POINT('Ctrl Pts',(64.8879780992218,8.37088331138052,-6.61723279487663));
#4986=CARTESIAN_POINT('Ctrl Pts',(64.8016959801978,8.56964482384595,-6.50148776616156));
#4987=CARTESIAN_POINT('Ctrl Pts',(64.7397191574786,8.67483765537062,-6.46423309101336));
#4988=CARTESIAN_POINT('Ctrl Pts',(64.6317941862906,8.8329346878098,-6.43134752238259));
#4989=CARTESIAN_POINT('Ctrl Pts',(64.5841440169343,8.89673206627378,-6.42446644642647));
#4990=CARTESIAN_POINT('Ctrl Pts',(64.5333054217746,8.9599013972947,-6.42360804569851));
#4991=CARTESIAN_POINT('',(65.0333054217745,7.98874638935144,-7.59753279036232));
#4992=CARTESIAN_POINT('Origin',(65.0333054217745,6.8454170790433,-9.42190830567978));
#4993=CARTESIAN_POINT('',(58.5152881956451,7.08092325871652,-8.45003545425543));
#4994=CARTESIAN_POINT('',(58.5152881956451,5.84833565888647,-9.34556276502401));
#4995=CARTESIAN_POINT('Ctrl Pts',(58.5152881956451,7.08092325871652,-8.45003545425542));
#4996=CARTESIAN_POINT('Ctrl Pts',(58.4654152249681,7.01988302569362,-8.43524406249618));
#4997=CARTESIAN_POINT('Ctrl Pts',(58.4186772780868,6.95679078914847,-8.42607245779616));
#4998=CARTESIAN_POINT('Ctrl Pts',(58.3120945049187,6.79559839891971,-8.41841231310071));
#4999=CARTESIAN_POINT('Ctrl Pts',(58.2507030237862,6.68411965386863,-8.42829926704623));
#5000=CARTESIAN_POINT('Ctrl Pts',(58.1653214105115,6.46237728512112,-8.49101819079154));
#5001=CARTESIAN_POINT('Ctrl Pts',(58.1417842183134,6.35206228988776,-8.54428356389661));
#5002=CARTESIAN_POINT('Ctrl Pts',(58.1417842183134,6.16320136361389,-8.68149905871306));
#5003=CARTESIAN_POINT('Ctrl Pts',(58.1653214105115,6.07845377516792,-8.76995494827363));
#5004=CARTESIAN_POINT('Ctrl Pts',(58.2507030237862,5.95028237372899,-8.96146325970346));
#5005=CARTESIAN_POINT('Ctrl Pts',(58.3120945049187,5.90643049502042,-9.06443060982093));
#5006=CARTESIAN_POINT('Ctrl Pts',(58.4186772780868,5.86390453760418,-9.22010079781545));
#5007=CARTESIAN_POINT('Ctrl Pts',(58.4654152249681,5.85313067871345,-9.28293926222734));
#5008=CARTESIAN_POINT('Ctrl Pts',(58.5152881956451,5.84833565888646,-9.34556276502401));
#5009=CARTESIAN_POINT('',(64.5333054217746,7.08092325871652,-8.45003545425543));
#5010=CARTESIAN_POINT('',(65.0333054217745,7.08092325871653,-8.45003545425542));
#5011=CARTESIAN_POINT('',(64.5333054217746,5.84833565888647,-9.34556276502401));
#5012=CARTESIAN_POINT('Ctrl Pts',(64.5333054217746,5.84833565888646,-9.34556276502401));
#5013=CARTESIAN_POINT('Ctrl Pts',(64.5841440169343,5.85315880086979,-9.28257198367587));
#5014=CARTESIAN_POINT('Ctrl Pts',(64.6317941862906,5.86403216913269,-9.21933256109938));
#5015=CARTESIAN_POINT('Ctrl Pts',(64.7397191574786,5.90677984040867,-9.06361239897923));
#5016=CARTESIAN_POINT('Ctrl Pts',(64.8016959801978,5.95056611450767,-8.96096638188601));
#5017=CARTESIAN_POINT('Ctrl Pts',(64.8879780992218,6.07856308547815,-8.76986477034863));
#5018=CARTESIAN_POINT('Ctrl Pts',(64.9118211190309,6.16320972496414,-8.68149298383651));
#5019=CARTESIAN_POINT('Ctrl Pts',(64.9118211190309,6.35205392853751,-8.54428963877316));
#5020=CARTESIAN_POINT('Ctrl Pts',(64.8879780992218,6.4622577420744,-8.49109428456304));
#5021=CARTESIAN_POINT('Ctrl Pts',(64.8016959801978,6.68355941425992,-8.42841557687301));
#5022=CARTESIAN_POINT('Ctrl Pts',(64.7397191574786,6.79471228050513,-8.41849171925358));
#5023=CARTESIAN_POINT('Ctrl Pts',(64.6317941862906,6.95602071230226,-8.42595644439207));
#5024=CARTESIAN_POINT('Ctrl Pts',(64.5841440169343,7.01952503280972,-8.43515731294215));
#5025=CARTESIAN_POINT('Ctrl Pts',(64.5333054217746,7.08092325871652,-8.45003545425542));
#5026=CARTESIAN_POINT('',(65.0333054217745,5.84833565888646,-9.34556276502402));
#5027=CARTESIAN_POINT('Origin',(65.0333054217745,4.28722240024657,-10.8282877315631));
#5028=CARTESIAN_POINT('',(58.5152881956451,4.75702466997909,-9.94551605816494));
#5029=CARTESIAN_POINT('',(58.5152881956451,3.34045249029966,-10.5063766605837));
#5030=CARTESIAN_POINT('Ctrl Pts',(58.5152881956451,4.7570246699791,-9.94551605816493));
#5031=CARTESIAN_POINT('Ctrl Pts',(58.4654152249681,4.70158059766936,-9.91600927651429));
#5032=CARTESIAN_POINT('Ctrl Pts',(58.4186772780868,4.64275140509176,-9.89143541345394));
#5033=CARTESIAN_POINT('Ctrl Pts',(58.3120945049187,4.48852817073407,-9.84392900895229));
#5034=CARTESIAN_POINT('Ctrl Pts',(58.2507030237862,4.37809294999274,-9.82578170953074));
#5035=CARTESIAN_POINT('Ctrl Pts',(58.1653214105115,4.1477194634458,-9.83138511829107));
#5036=CARTESIAN_POINT('Ctrl Pts',(58.1417842183134,4.02762365701549,-9.8555428380347));
#5037=CARTESIAN_POINT('Ctrl Pts',(58.1417842183134,3.81057203810829,-9.94147965331495));
#5038=CARTESIAN_POINT('Ctrl Pts',(58.1653214105115,3.70648886579938,-10.0060806702378));
#5039=CARTESIAN_POINT('Ctrl Pts',(58.2507030237862,3.53471802426675,-10.1596974645434));
#5040=CARTESIAN_POINT('Ctrl Pts',(58.3120945049187,3.46663689428341,-10.2485243872452));
#5041=CARTESIAN_POINT('Ctrl Pts',(58.4186772780868,3.38673336653187,-10.388728134475));
#5042=CARTESIAN_POINT('Ctrl Pts',(58.4654152249681,3.36067069760572,-10.4469130632236));
#5043=CARTESIAN_POINT('Ctrl Pts',(58.5152881956451,3.34045249029966,-10.5063766605837));
#5044=CARTESIAN_POINT('',(64.5333054217746,4.75702466997909,-9.94551605816494));
#5045=CARTESIAN_POINT('',(65.0333054217745,4.7570246699791,-9.94551605816493));
#5046=CARTESIAN_POINT('',(64.5333054217746,3.34045249029966,-10.5063766605837));
#5047=CARTESIAN_POINT('Ctrl Pts',(64.5333054217746,3.34045249029966,-10.5063766605837));
#5048=CARTESIAN_POINT('Ctrl Pts',(64.5841440169343,3.36078927471434,-10.4465643170991));
#5049=CARTESIAN_POINT('Ctrl Pts',(64.6317941862906,3.38704804098346,-10.3880157739984));
#5050=CARTESIAN_POINT('Ctrl Pts',(64.7397191574787,3.46717874510578,-10.2478187606668));
#5051=CARTESIAN_POINT('Ctrl Pts',(64.8016959801978,3.53511641929548,-10.1592867605185));
#5052=CARTESIAN_POINT('Ctrl Pts',(64.8879780992218,3.7066171682632,-10.0060205097869));
#5053=CARTESIAN_POINT('Ctrl Pts',(64.911821119031,3.81058164753171,-9.94147584867507));
#5054=CARTESIAN_POINT('Ctrl Pts',(64.911821119031,4.02761404759207,-9.85554664267458));
#5055=CARTESIAN_POINT('Ctrl Pts',(64.8879780992218,4.14758475231227,-9.83142909229001));
#5056=CARTESIAN_POINT('Ctrl Pts',(64.8016959801978,4.37752138626385,-9.82575503934536));
#5057=CARTESIAN_POINT('Ctrl Pts',(64.7397191574786,4.48765014385175,-9.84378555172631));
#5058=CARTESIAN_POINT('Ctrl Pts',(64.6317941862906,4.64203437298612,-9.89113153450027));
#5059=CARTESIAN_POINT('Ctrl Pts',(64.5841440169343,4.70125542552701,-9.91583622314711));
#5060=CARTESIAN_POINT('Ctrl Pts',(64.5333054217746,4.7570246699791,-9.94551605816493));
#5061=CARTESIAN_POINT('',(65.0333054217745,3.34045249029966,-10.5063766605837));
#5062=CARTESIAN_POINT('Origin',(65.0333054217745,1.45964577074129,-11.5542860156157));
#5063=CARTESIAN_POINT('',(58.5152881956451,2.13422472611394,-10.8160833110905));
#5064=CARTESIAN_POINT('',(58.5152881956451,0.622676406422437,-11.0070362708084));
#5065=CARTESIAN_POINT('Ctrl Pts',(58.5152881956451,2.13422472611394,-10.8160833110905));
#5066=CARTESIAN_POINT('Ctrl Pts',(58.4654152249681,2.08786056948963,-10.7737151591579));
#5067=CARTESIAN_POINT('Ctrl Pts',(58.4186772780868,2.03699087540786,-10.7352831039296));
#5068=CARTESIAN_POINT('Ctrl Pts',(58.3120945049187,1.89942720992933,-10.650915441733));
#5069=CARTESIAN_POINT('Ctrl Pts',(58.2507030237862,1.79697456456924,-10.6058741505081));
#5070=CARTESIAN_POINT('Ctrl Pts',(58.1653214105115,1.57244517363704,-10.5540099615032));
#5071=CARTESIAN_POINT('Ctrl Pts',(58.1417842183134,1.45011461720928,-10.547542109508));
#5072=CARTESIAN_POINT('Ctrl Pts',(58.1417842183134,1.2185104571447,-10.5768005190945));
#5073=CARTESIAN_POINT('Ctrl Pts',(58.1653214105115,1.10163162948015,-10.6134875439005));
#5074=CARTESIAN_POINT('Ctrl Pts',(58.2507030237862,0.897054341556291,-10.7195605129324));
#5075=CARTESIAN_POINT('Ctrl Pts',(58.3120945049187,0.809021748079895,-10.7886656859827));
#5076=CARTESIAN_POINT('Ctrl Pts',(58.4186772780868,0.696761282506315,-10.904593475376));
#5077=CARTESIAN_POINT('Ctrl Pts',(58.4654152249681,0.657047416885181,-10.9544688953989));
#5078=CARTESIAN_POINT('Ctrl Pts',(58.5152881956451,0.622676406422432,-11.0070362708084));
#5079=CARTESIAN_POINT('',(64.5333054217746,2.13422472611394,-10.8160833110905));
#5080=CARTESIAN_POINT('',(65.0333054217745,2.13422472611395,-10.8160833110905));
#5081=CARTESIAN_POINT('',(64.5333054217746,0.622676406422437,-11.0070362708084));
#5082=CARTESIAN_POINT('Ctrl Pts',(64.5333054217746,0.622676406422433,-11.0070362708084));
#5083=CARTESIAN_POINT('Ctrl Pts',(64.5841440169343,0.657248998310229,-10.954160594703));
#5084=CARTESIAN_POINT('Ctrl Pts',(64.6317941862906,0.697243227727885,-10.9039817513676));
#5085=CARTESIAN_POINT('Ctrl Pts',(64.7397191574786,0.809722057856438,-10.7881169807807));
#5086=CARTESIAN_POINT('Ctrl Pts',(64.8016959801978,0.897542358210194,-10.7192617887444));
#5087=CARTESIAN_POINT('Ctrl Pts',(64.8879780992218,1.10177086238189,-10.613461181026));
#5088=CARTESIAN_POINT('Ctrl Pts',(64.9118211190309,1.21852071084588,-10.5767992237508));
#5089=CARTESIAN_POINT('Ctrl Pts',(64.9118211190309,1.4501043635081,-10.5475434048517));
#5090=CARTESIAN_POINT('Ctrl Pts',(64.8879780992218,1.57230375881265,-10.5540190526815));
#5091=CARTESIAN_POINT('Ctrl Pts',(64.8016959801978,1.79642759017132,-10.6057061760964));
#5092=CARTESIAN_POINT('Ctrl Pts',(64.7397191574786,1.89861244423744,-10.6505581350733));
#5093=CARTESIAN_POINT('Ctrl Pts',(64.6317941862906,2.03637194180704,-10.7348104532587));
#5094=CARTESIAN_POINT('Ctrl Pts',(64.5841440169343,2.08758864985044,-10.7734666755571));
#5095=CARTESIAN_POINT('Ctrl Pts',(64.5333054217746,2.13422472611394,-10.8160833110905));
#5096=CARTESIAN_POINT('',(65.0333054217745,0.622676406422429,-11.0070362708084));
#5097=CARTESIAN_POINT('Origin',(65.0333054217745,-1.45964577074129,-11.5542860156157));
#5098=CARTESIAN_POINT('',(58.5152881956451,-0.622676406422435,-11.0070362708084));
#5099=CARTESIAN_POINT('',(58.5152881956451,-2.13422472611394,-10.8160833110905));
#5100=CARTESIAN_POINT('Ctrl Pts',(58.5152881956451,-0.62267640642243,-11.0070362708084));
#5101=CARTESIAN_POINT('Ctrl Pts',(58.4654152249681,-0.657047416885175,-10.9544688953989));
#5102=CARTESIAN_POINT('Ctrl Pts',(58.4186772780868,-0.696761282506316,-10.904593475376));
#5103=CARTESIAN_POINT('Ctrl Pts',(58.3120945049187,-0.809021748079893,-10.7886656859827));
#5104=CARTESIAN_POINT('Ctrl Pts',(58.2507030237862,-0.897054341556289,-10.7195605129324));
#5105=CARTESIAN_POINT('Ctrl Pts',(58.1653214105115,-1.10163162948015,-10.6134875439005));
#5106=CARTESIAN_POINT('Ctrl Pts',(58.1417842183134,-1.2185104571447,-10.5768005190945));
#5107=CARTESIAN_POINT('Ctrl Pts',(58.1417842183134,-1.45011461720927,-10.547542109508));
#5108=CARTESIAN_POINT('Ctrl Pts',(58.1653214105115,-1.57244517363704,-10.5540099615032));
#5109=CARTESIAN_POINT('Ctrl Pts',(58.2507030237862,-1.79697456456924,-10.6058741505081));
#5110=CARTESIAN_POINT('Ctrl Pts',(58.3120945049187,-1.89942720992933,-10.650915441733));
#5111=CARTESIAN_POINT('Ctrl Pts',(58.4186772780868,-2.03699087540785,-10.7352831039296));
#5112=CARTESIAN_POINT('Ctrl Pts',(58.4654152249681,-2.08786056948963,-10.7737151591579));
#5113=CARTESIAN_POINT('Ctrl Pts',(58.5152881956451,-2.13422472611394,-10.8160833110905));
#5114=CARTESIAN_POINT('',(64.5333054217746,-0.622676406422435,-11.0070362708084));
#5115=CARTESIAN_POINT('',(65.0333054217745,-0.622676406422428,-11.0070362708084));
#5116=CARTESIAN_POINT('',(64.5333054217746,-2.13422472611394,-10.8160833110905));
#5117=CARTESIAN_POINT('Ctrl Pts',(64.5333054217746,-2.13422472611394,-10.8160833110905));
#5118=CARTESIAN_POINT('Ctrl Pts',(64.5841440169343,-2.08758864985044,-10.7734666755571));
#5119=CARTESIAN_POINT('Ctrl Pts',(64.6317941862906,-2.03637194180704,-10.7348104532587));
#5120=CARTESIAN_POINT('Ctrl Pts',(64.7397191574786,-1.89861244423744,-10.6505581350733));
#5121=CARTESIAN_POINT('Ctrl Pts',(64.8016959801978,-1.79642759017132,-10.6057061760964));
#5122=CARTESIAN_POINT('Ctrl Pts',(64.8879780992218,-1.57230375881265,-10.5540190526815));
#5123=CARTESIAN_POINT('Ctrl Pts',(64.9118211190309,-1.45010436350809,-10.5475434048517));
#5124=CARTESIAN_POINT('Ctrl Pts',(64.9118211190309,-1.21852071084588,-10.5767992237508));
#5125=CARTESIAN_POINT('Ctrl Pts',(64.8879780992218,-1.10177086238189,-10.613461181026));
#5126=CARTESIAN_POINT('Ctrl Pts',(64.8016959801978,-0.897542358210193,-10.7192617887444));
#5127=CARTESIAN_POINT('Ctrl Pts',(64.7397191574786,-0.809722057856437,-10.7881169807807));
#5128=CARTESIAN_POINT('Ctrl Pts',(64.6317941862906,-0.697243227727883,-10.9039817513676));
#5129=CARTESIAN_POINT('Ctrl Pts',(64.5841440169343,-0.657248998310227,-10.954160594703));
#5130=CARTESIAN_POINT('Ctrl Pts',(64.5333054217746,-0.622676406422431,-11.0070362708084));
#5131=CARTESIAN_POINT('',(65.0333054217745,-2.13422472611394,-10.8160833110905));
#5132=CARTESIAN_POINT('Origin',(65.0333054217745,-4.28722240024656,-10.8282877315631));
#5133=CARTESIAN_POINT('',(58.5152881956451,-3.34045249029966,-10.5063766605837));
#5134=CARTESIAN_POINT('',(58.5152881956451,-4.75702466997909,-9.94551605816494));
#5135=CARTESIAN_POINT('Ctrl Pts',(58.5152881956451,-3.34045249029965,-10.5063766605837));
#5136=CARTESIAN_POINT('Ctrl Pts',(58.4654152249681,-3.36067069760572,-10.4469130632236));
#5137=CARTESIAN_POINT('Ctrl Pts',(58.4186772780868,-3.38673336653187,-10.388728134475));
#5138=CARTESIAN_POINT('Ctrl Pts',(58.3120945049187,-3.4666368942834,-10.2485243872452));
#5139=CARTESIAN_POINT('Ctrl Pts',(58.2507030237862,-3.53471802426675,-10.1596974645434));
#5140=CARTESIAN_POINT('Ctrl Pts',(58.1653214105115,-3.70648886579937,-10.0060806702378));
#5141=CARTESIAN_POINT('Ctrl Pts',(58.1417842183134,-3.81057203810828,-9.94147965331495));
#5142=CARTESIAN_POINT('Ctrl Pts',(58.1417842183134,-4.02762365701548,-9.8555428380347));
#5143=CARTESIAN_POINT('Ctrl Pts',(58.1653214105115,-4.1477194634458,-9.83138511829107));
#5144=CARTESIAN_POINT('Ctrl Pts',(58.2507030237862,-4.37809294999273,-9.82578170953074));
#5145=CARTESIAN_POINT('Ctrl Pts',(58.3120945049187,-4.48852817073407,-9.84392900895229));
#5146=CARTESIAN_POINT('Ctrl Pts',(58.4186772780868,-4.64275140509175,-9.89143541345394));
#5147=CARTESIAN_POINT('Ctrl Pts',(58.4654152249681,-4.70158059766935,-9.91600927651429));
#5148=CARTESIAN_POINT('Ctrl Pts',(58.5152881956451,-4.75702466997909,-9.94551605816493));
#5149=CARTESIAN_POINT('',(64.5333054217746,-3.34045249029966,-10.5063766605837));
#5150=CARTESIAN_POINT('',(65.0333054217745,-3.34045249029965,-10.5063766605837));
#5151=CARTESIAN_POINT('',(64.5333054217746,-4.75702466997909,-9.94551605816494));
#5152=CARTESIAN_POINT('Ctrl Pts',(64.5333054217746,-4.75702466997909,-9.94551605816493));
#5153=CARTESIAN_POINT('Ctrl Pts',(64.5841440169343,-4.70125542552701,-9.91583622314712));
#5154=CARTESIAN_POINT('Ctrl Pts',(64.6317941862906,-4.64203437298611,-9.89113153450027));
#5155=CARTESIAN_POINT('Ctrl Pts',(64.7397191574786,-4.48765014385175,-9.84378555172631));
#5156=CARTESIAN_POINT('Ctrl Pts',(64.8016959801978,-4.37752138626384,-9.82575503934536));
#5157=CARTESIAN_POINT('Ctrl Pts',(64.8879780992218,-4.14758475231227,-9.83142909229001));
#5158=CARTESIAN_POINT('Ctrl Pts',(64.911821119031,-4.02761404759206,-9.85554664267458));
#5159=CARTESIAN_POINT('Ctrl Pts',(64.911821119031,-3.81058164753171,-9.94147584867507));
#5160=CARTESIAN_POINT('Ctrl Pts',(64.8879780992218,-3.70661716826319,-10.0060205097869));
#5161=CARTESIAN_POINT('Ctrl Pts',(64.8016959801978,-3.53511641929547,-10.1592867605185));
#5162=CARTESIAN_POINT('Ctrl Pts',(64.7397191574786,-3.46717874510578,-10.2478187606668));
#5163=CARTESIAN_POINT('Ctrl Pts',(64.6317941862906,-3.38704804098345,-10.3880157739984));
#5164=CARTESIAN_POINT('Ctrl Pts',(64.5841440169343,-3.36078927471433,-10.4465643170991));
#5165=CARTESIAN_POINT('Ctrl Pts',(64.5333054217746,-3.34045249029965,-10.5063766605837));
#5166=CARTESIAN_POINT('',(65.0333054217745,-4.7570246699791,-9.94551605816494));
#5167=CARTESIAN_POINT('Origin',(65.0333054217745,-6.8454170790433,-9.42190830567978));
#5168=CARTESIAN_POINT('',(58.5152881956451,-5.84833565888647,-9.34556276502401));
#5169=CARTESIAN_POINT('',(58.5152881956451,-7.08092325871652,-8.45003545425543));
#5170=CARTESIAN_POINT('Ctrl Pts',(58.5152881956451,-5.84833565888646,-9.34556276502402));
#5171=CARTESIAN_POINT('Ctrl Pts',(58.4654152249681,-5.85313067871344,-9.28293926222734));
#5172=CARTESIAN_POINT('Ctrl Pts',(58.4186772780868,-5.86390453760418,-9.22010079781545));
#5173=CARTESIAN_POINT('Ctrl Pts',(58.3120945049187,-5.90643049502042,-9.06443060982092));
#5174=CARTESIAN_POINT('Ctrl Pts',(58.2507030237862,-5.95028237372899,-8.96146325970346));
#5175=CARTESIAN_POINT('Ctrl Pts',(58.1653214105115,-6.07845377516792,-8.76995494827363));
#5176=CARTESIAN_POINT('Ctrl Pts',(58.1417842183134,-6.16320136361389,-8.68149905871306));
#5177=CARTESIAN_POINT('Ctrl Pts',(58.1417842183134,-6.35206228988776,-8.54428356389661));
#5178=CARTESIAN_POINT('Ctrl Pts',(58.1653214105115,-6.46237728512112,-8.49101819079154));
#5179=CARTESIAN_POINT('Ctrl Pts',(58.2507030237862,-6.68411965386863,-8.42829926704623));
#5180=CARTESIAN_POINT('Ctrl Pts',(58.3120945049187,-6.7955983989197,-8.41841231310071));
#5181=CARTESIAN_POINT('Ctrl Pts',(58.4186772780868,-6.95679078914847,-8.42607245779616));
#5182=CARTESIAN_POINT('Ctrl Pts',(58.4654152249681,-7.01988302569362,-8.43524406249618));
#5183=CARTESIAN_POINT('Ctrl Pts',(58.5152881956451,-7.08092325871652,-8.45003545425542));
#5184=CARTESIAN_POINT('',(64.5333054217746,-5.84833565888647,-9.34556276502401));
#5185=CARTESIAN_POINT('',(65.0333054217745,-5.84833565888646,-9.34556276502402));
#5186=CARTESIAN_POINT('',(64.5333054217746,-7.08092325871652,-8.45003545425543));
#5187=CARTESIAN_POINT('Ctrl Pts',(64.5333054217746,-7.08092325871652,-8.45003545425542));
#5188=CARTESIAN_POINT('Ctrl Pts',(64.5841440169343,-7.01952503280971,-8.43515731294215));
#5189=CARTESIAN_POINT('Ctrl Pts',(64.6317941862906,-6.95602071230226,-8.42595644439207));
#5190=CARTESIAN_POINT('Ctrl Pts',(64.7397191574786,-6.79471228050513,-8.41849171925358));
#5191=CARTESIAN_POINT('Ctrl Pts',(64.8016959801978,-6.68355941425992,-8.42841557687302));
#5192=CARTESIAN_POINT('Ctrl Pts',(64.8879780992218,-6.4622577420744,-8.49109428456304));
#5193=CARTESIAN_POINT('Ctrl Pts',(64.911821119031,-6.35205392853751,-8.54428963877316));
#5194=CARTESIAN_POINT('Ctrl Pts',(64.911821119031,-6.16320972496414,-8.68149298383651));
#5195=CARTESIAN_POINT('Ctrl Pts',(64.8879780992218,-6.07856308547815,-8.76986477034863));
#5196=CARTESIAN_POINT('Ctrl Pts',(64.8016959801978,-5.95056611450767,-8.96096638188601));
#5197=CARTESIAN_POINT('Ctrl Pts',(64.7397191574786,-5.90677984040867,-9.06361239897923));
#5198=CARTESIAN_POINT('Ctrl Pts',(64.6317941862906,-5.86403216913269,-9.21933256109938));
#5199=CARTESIAN_POINT('Ctrl Pts',(64.5841440169343,-5.85315880086979,-9.28257198367587));
#5200=CARTESIAN_POINT('Ctrl Pts',(64.5333054217746,-5.84833565888646,-9.34556276502402));
#5201=CARTESIAN_POINT('',(65.0333054217745,-7.08092325871653,-8.45003545425542));
#5202=CARTESIAN_POINT('Origin',(65.0333054217745,-8.97348902708079,-7.42351572959578));
#5203=CARTESIAN_POINT('',(58.5152881956451,-7.98874638935144,-7.59753279036232));
#5204=CARTESIAN_POINT('',(58.5152881956451,-8.9599013972947,-6.42360804569852));
#5205=CARTESIAN_POINT('Ctrl Pts',(58.5152881956451,-7.98874638935143,-7.59753279036232));
#5206=CARTESIAN_POINT('Ctrl Pts',(58.4654152249681,-7.97781693296876,-7.53568424712285));
#5207=CARTESIAN_POINT('Ctrl Pts',(58.4186772780868,-7.9726250206465,-7.47214061887045));
#5208=CARTESIAN_POINT('Ctrl Pts',(58.3120945049187,-7.97510134542344,-7.31078532053779));
#5209=CARTESIAN_POINT('Ctrl Pts',(58.2507030237862,-7.99196859804204,-7.20014736029998));
#5210=CARTESIAN_POINT('Ctrl Pts',(58.1653214105115,-8.06848707885343,-6.98278070327126));
#5211=CARTESIAN_POINT('Ctrl Pts',(58.1417842183134,-8.12857408077458,-6.87602794993212));
#5212=CARTESIAN_POINT('Ctrl Pts',(58.1417842183134,-8.27737748783543,-6.69615552976207));
#5213=CARTESIAN_POINT('Ctrl Pts',(58.1653214105115,-8.37098017501116,-6.61712936258409));
#5214=CARTESIAN_POINT('Ctrl Pts',(58.2507030237862,-8.57015853741945,-6.50123578449678));
#5215=CARTESIAN_POINT('Ctrl Pts',(58.3120945049187,-8.67567618723855,-6.46393581086227));
#5216=CARTESIAN_POINT('Ctrl Pts',(58.4186772780868,-8.8337094226362,-6.43126838068827));
#5217=CARTESIAN_POINT('Ctrl Pts',(58.4654152249681,-8.89710038588973,-6.42446144137384));
#5218=CARTESIAN_POINT('Ctrl Pts',(58.5152881956451,-8.9599013972947,-6.42360804569852));
#5219=CARTESIAN_POINT('',(64.5333054217746,-7.98874638935144,-7.59753279036232));
#5220=CARTESIAN_POINT('',(65.0333054217745,-7.98874638935143,-7.59753279036232));
#5221=CARTESIAN_POINT('',(64.5333054217746,-8.9599013972947,-6.42360804569852));
#5222=CARTESIAN_POINT('Ctrl Pts',(64.5333054217746,-8.9599013972947,-6.42360804569852));
#5223=CARTESIAN_POINT('Ctrl Pts',(64.5841440169343,-8.89673206627377,-6.42446644642648));
#5224=CARTESIAN_POINT('Ctrl Pts',(64.6317941862906,-8.83293468780981,-6.43134752238259));
#5225=CARTESIAN_POINT('Ctrl Pts',(64.7397191574786,-8.67483765537062,-6.46423309101336));
#5226=CARTESIAN_POINT('Ctrl Pts',(64.8016959801978,-8.56964482384596,-6.50148776616156));
#5227=CARTESIAN_POINT('Ctrl Pts',(64.8879780992218,-8.37088331138052,-6.61723279487663));
#5228=CARTESIAN_POINT('Ctrl Pts',(64.9118211190309,-8.27737089993273,-6.69616349316846));
#5229=CARTESIAN_POINT('Ctrl Pts',(64.9118211190309,-8.12858066867727,-6.87601998652574));
#5230=CARTESIAN_POINT('Ctrl Pts',(64.8879780992218,-8.06857052864127,-6.98266617408288));
#5231=CARTESIAN_POINT('Ctrl Pts',(64.8016959801978,-7.99211985609405,-7.19959552935062));
#5232=CARTESIAN_POINT('Ctrl Pts',(64.7397191574786,-7.97523623472202,-7.30990593662909));
#5233=CARTESIAN_POINT('Ctrl Pts',(64.6317941862906,-7.9725575896936,-7.47136477705307));
#5234=CARTESIAN_POINT('Ctrl Pts',(64.5841440169343,-7.97775283315432,-7.53532151360656));
#5235=CARTESIAN_POINT('Ctrl Pts',(64.5333054217746,-7.98874638935143,-7.59753279036232));
#5236=CARTESIAN_POINT('',(65.0333054217745,-8.9599013972947,-6.42360804569852));
#5237=CARTESIAN_POINT('Origin',(65.0333054217745,-10.5377236573627,-4.95867635844022));
#5238=CARTESIAN_POINT('',(58.5152881956451,-9.62719480361945,-5.37212188871111));
#5239=CARTESIAN_POINT('',(58.5152881956451,-10.2758959788686,-3.99356171925254));
#5240=CARTESIAN_POINT('Ctrl Pts',(58.5152881956451,-9.62719480361944,-5.37212188871112));
#5241=CARTESIAN_POINT('Ctrl Pts',(58.4654152249681,-9.60122760896735,-5.31493447646361));
#5242=CARTESIAN_POINT('Ctrl Pts',(58.4186772780868,-9.58039615237782,-5.25467836423091));
#5243=CARTESIAN_POINT('Ctrl Pts',(58.3120945049187,-9.54266724792246,-5.09777650237765));
#5244=CARTESIAN_POINT('Ctrl Pts',(58.2507030237862,-9.53149004293564,-4.98641972195919));
#5245=CARTESIAN_POINT('Ctrl Pts',(58.1653214105115,-9.55154766555483,-4.75685266581133));
#5246=CARTESIAN_POINT('Ctrl Pts',(58.1417842183134,-9.5831985936359,-4.63851071679508));
#5247=CARTESIAN_POINT('Ctrl Pts',(58.1417842183134,-9.68259461615746,-4.42728341695521));
#5248=CARTESIAN_POINT('Ctrl Pts',(58.1653214105115,-9.75360359419369,-4.32746196042602));
#5249=CARTESIAN_POINT('Ctrl Pts',(58.2507030237862,-9.91770284122587,-4.16567574773471));
#5250=CARTESIAN_POINT('Ctrl Pts',(58.3120945049187,-10.0106293338081,-4.10330644893437));
#5251=CARTESIAN_POINT('Ctrl Pts',(58.4186772780868,-10.155573604989,-4.03236405867115));
#5252=CARTESIAN_POINT('Ctrl Pts',(58.4654152249681,-10.2152802075941,-4.01000628037358));
#5253=CARTESIAN_POINT('Ctrl Pts',(58.5152881956451,-10.2758959788686,-3.99356171925254));
#5254=CARTESIAN_POINT('',(64.5333054217746,-9.62719480361945,-5.37212188871111));
#5255=CARTESIAN_POINT('',(65.0333054217745,-9.62719480361944,-5.37212188871112));
#5256=CARTESIAN_POINT('',(64.5333054217746,-10.2758959788686,-3.99356171925254));
#5257=CARTESIAN_POINT('Ctrl Pts',(64.5333054217746,-10.2758959788686,-3.99356171925254));
#5258=CARTESIAN_POINT('Ctrl Pts',(64.5841440169343,-10.2149247041221,-4.01010272554701));
#5259=CARTESIAN_POINT('Ctrl Pts',(64.6317941862906,-10.1548428916209,-4.03263338270016));
#5260=CARTESIAN_POINT('Ctrl Pts',(64.7397191574786,-10.009891076528,-4.10380292387847));
#5261=CARTESIAN_POINT('Ctrl Pts',(64.8016959801978,-9.91726793220072,-4.16604756830275));
#5262=CARTESIAN_POINT('Ctrl Pts',(64.8879780992218,-9.75353549627729,-4.32758623220827));
#5263=CARTESIAN_POINT('Ctrl Pts',(64.9118211190309,-9.68259021564447,-4.42729276852132));
#5264=CARTESIAN_POINT('Ctrl Pts',(64.9118211190309,-9.58320299414888,-4.63850136522897));
#5265=CARTESIAN_POINT('Ctrl Pts',(64.8879780992218,-9.55160001136319,-4.75672098164969));
#5266=CARTESIAN_POINT('Ctrl Pts',(64.8016959801978,-9.53149931416127,-4.98584761144596));
#5267=CARTESIAN_POINT('Ctrl Pts',(64.7397191574786,-9.54257920554065,-5.09689120032706));
#5268=CARTESIAN_POINT('Ctrl Pts',(64.6317941862906,-9.58013789587828,-5.25394366630696));
#5269=CARTESIAN_POINT('Ctrl Pts',(64.5841440169343,-9.60107531480922,-5.31459907986337));
#5270=CARTESIAN_POINT('Ctrl Pts',(64.5333054217746,-9.62719480361944,-5.37212188871112));
#5271=CARTESIAN_POINT('',(65.0333054217745,-10.2758959788686,-3.99356171925253));
#5272=CARTESIAN_POINT('Origin',(65.0333054217745,-11.4398343552159,-2.18226511494789));
#5273=CARTESIAN_POINT('',(58.5152881956451,-10.6607311620303,-2.80916081150993));
#5274=CARTESIAN_POINT('',(58.5152881956451,-10.9462182239883,-1.31258522269331));
#5275=CARTESIAN_POINT('Ctrl Pts',(58.5152881956451,-10.6607311620303,-2.80916081150993));
#5276=CARTESIAN_POINT('Ctrl Pts',(58.4654152249681,-10.6213578434494,-2.76022782568649));
#5277=CARTESIAN_POINT('Ctrl Pts',(58.4186772780868,-10.5861957596229,-2.70704534261154));
#5278=CARTESIAN_POINT('Ctrl Pts',(58.3120945049187,-10.5106322717593,-2.56445563826261));
#5279=CARTESIAN_POINT('Ctrl Pts',(58.2507030237862,-10.4721129140633,-2.45937699371878));
#5280=CARTESIAN_POINT('Ctrl Pts',(58.1653214105115,-10.4344493842944,-2.23203408087814));
#5281=CARTESIAN_POINT('Ctrl Pts',(58.1417842183134,-10.4356754943201,-2.10953879607271));
#5282=CARTESIAN_POINT('Ctrl Pts',(58.1417842183134,-10.4794187146543,-1.88022880465162));
#5283=CARTESIAN_POINT('Ctrl Pts',(58.1653214105115,-10.5233722283083,-1.76588420800258));
#5284=CARTESIAN_POINT('Ctrl Pts',(58.2507030237862,-10.6420814007585,-1.56837098345874));
#5285=CARTESIAN_POINT('Ctrl Pts',(58.3120945049187,-10.7165778228152,-1.48485125191443));
#5286=CARTESIAN_POINT('Ctrl Pts',(58.4186772780868,-10.8393257481533,-1.38009147285009));
#5287=CARTESIAN_POINT('Ctrl Pts',(58.4654152249681,-10.8915964046827,-1.34358767700596));
#5288=CARTESIAN_POINT('Ctrl Pts',(58.5152881956451,-10.9462182239883,-1.31258522269331));
#5289=CARTESIAN_POINT('',(64.5333054217746,-10.6607311620303,-2.80916081150993));
#5290=CARTESIAN_POINT('',(65.0333054217746,-10.6607311620303,-2.80916081150993));
#5291=CARTESIAN_POINT('',(64.5333054217746,-10.9462182239883,-1.31258522269331));
#5292=CARTESIAN_POINT('Ctrl Pts',(64.5333054217746,-10.9462182239883,-1.31258522269331));
#5293=CARTESIAN_POINT('Ctrl Pts',(64.5841440169343,-10.8912760549453,-1.34376950229525));
#5294=CARTESIAN_POINT('Ctrl Pts',(64.6317941862906,-10.8386849696517,-1.38053405659456));
#5295=CARTESIAN_POINT('Ctrl Pts',(64.7397191574786,-10.7159862275429,-1.4855157263049));
#5296=CARTESIAN_POINT('Ctrl Pts',(64.8016959801978,-10.6417526232152,-1.5688392800763));
#5297=CARTESIAN_POINT('Ctrl Pts',(64.8879780992218,-10.5233371749486,-1.76602151082142));
#5298=CARTESIAN_POINT('Ctrl Pts',(64.9118211190309,-10.4794167780314,-1.88023895678416));
#5299=CARTESIAN_POINT('Ctrl Pts',(64.9118211190309,-10.4356774309429,-2.10952864394017));
#5300=CARTESIAN_POINT('Ctrl Pts',(64.8879780992218,-10.4344673370436,-2.23189351594341));
#5301=CARTESIAN_POINT('Ctrl Pts',(64.8016959801978,-10.4719796159174,-2.45882055144931));
#5302=CARTESIAN_POINT('Ctrl Pts',(64.7397191574786,-10.5103268297238,-2.5636200448539));
#5303=CARTESIAN_POINT('Ctrl Pts',(64.6317941862906,-10.5857629047824,-2.70639795235363));
#5304=CARTESIAN_POINT('Ctrl Pts',(64.5841440169343,-10.6211269241497,-2.75994084020421));
#5305=CARTESIAN_POINT('Ctrl Pts',(64.5333054217746,-10.6607311620303,-2.80916081150993));
#5306=CARTESIAN_POINT('',(65.0333054217746,-10.9462182239883,-1.31258522269331));
#5307=CARTESIAN_POINT('Origin',(65.0333054217745,-11.6231381877631,0.731265871526303));
#5308=CARTESIAN_POINT('',(58.5152881956451,-11.0244145741041,-0.0696898291507972));
#5309=CARTESIAN_POINT('',(58.5152881956451,-10.9287493207203,1.45086583075851));
#5310=CARTESIAN_POINT('Ctrl Pts',(58.5152881956451,-11.0244145741041,-0.0696898291508038));
#5311=CARTESIAN_POINT('Ctrl Pts',(58.4654152249681,-10.9741091020059,-0.0320859092136465));
#5312=CARTESIAN_POINT('Ctrl Pts',(58.4186772780868,-10.9268257539862,0.0106812937004472));
#5313=CARTESIAN_POINT('Ctrl Pts',(58.3120945049187,-10.8181756145601,0.129999405012571));
#5314=CARTESIAN_POINT('Ctrl Pts',(58.2507030237862,-10.7547344170632,0.22219743599286));
#5315=CARTESIAN_POINT('Ctrl Pts',(58.1653214105115,-10.6617162729982,0.433031414203767));
#5316=CARTESIAN_POINT('Ctrl Pts',(58.1417842183134,-10.6324405239663,0.551983205547908));
#5317=CARTESIAN_POINT('Ctrl Pts',(58.1417842183134,-10.6177823947033,0.784967498446072));
#5318=CARTESIAN_POINT('Ctrl Pts',(58.1653214105115,-10.6319186830624,0.906650543677475));
#5319=CARTESIAN_POINT('Ctrl Pts',(58.2507030237862,-10.6977788470438,1.12748029777295));
#5320=CARTESIAN_POINT('Ctrl Pts',(58.3120945049187,-10.7491643143985,1.22690261016421));
#5321=CARTESIAN_POINT('Ctrl Pts',(58.4186772780868,-10.8420031903095,1.35889733583154));
#5322=CARTESIAN_POINT('Ctrl Pts',(58.4654152249681,-10.8835535431755,1.40725348147776));
#5323=CARTESIAN_POINT('Ctrl Pts',(58.5152881956451,-10.9287493207203,1.45086583075852));
#5324=CARTESIAN_POINT('',(64.5333054217746,-11.0244145741041,-0.0696898291507972));
#5325=CARTESIAN_POINT('',(65.0333054217745,-11.0244145741041,-0.0696898291508069));
#5326=CARTESIAN_POINT('',(64.5333054217746,-10.9287493207203,1.45086583075851));
#5327=CARTESIAN_POINT('Ctrl Pts',(64.5333054217746,-10.9287493207203,1.45086583075851));
#5328=CARTESIAN_POINT('Ctrl Pts',(64.5841440169343,-10.8832884759249,1.40699770082426));
#5329=CARTESIAN_POINT('Ctrl Pts',(64.6317941862906,-10.8414926091443,1.35830930153599));
#5330=CARTESIAN_POINT('Ctrl Pts',(64.7397191574786,-10.7487565532408,1.22611188769709));
#5331=CARTESIAN_POINT('Ctrl Pts',(64.8016959801978,-10.6975768592847,1.12694494990463));
#5332=CARTESIAN_POINT('Ctrl Pts',(64.8879780992218,-10.6319188767911,0.906508837063125));
#5333=CARTESIAN_POINT('Ctrl Pts',(64.911821119031,-10.6177830436557,0.784957183642927));
#5334=CARTESIAN_POINT('Ctrl Pts',(64.911821119031,-10.6324398750139,0.551993520351054));
#5335=CARTESIAN_POINT('Ctrl Pts',(64.8879780992218,-10.6616987046511,0.433172027699774));
#5336=CARTESIAN_POINT('Ctrl Pts',(64.8016959801978,-10.7544669251584,0.222703246704335));
#5337=CARTESIAN_POINT('Ctrl Pts',(64.7397191574786,-10.8176719649172,0.130732786372442));
#5338=CARTESIAN_POINT('Ctrl Pts',(64.6317941862906,-10.9262454986663,0.0112006983815039));
#5339=CARTESIAN_POINT('Ctrl Pts',(64.5841440169343,-10.9738140670733,-0.0318653672026201));
#5340=CARTESIAN_POINT('Ctrl Pts',(64.5333054217746,-11.0244145741041,-0.0696898291508038));
#5341=CARTESIAN_POINT('',(65.0333054217745,-10.9287493207203,1.45086583075852));
#5342=CARTESIAN_POINT('Origin',(65.0333054217745,-11.0761175010611,3.59884873388475));
#5343=CARTESIAN_POINT('',(58.5152881956451,-10.6953934735264,2.67416002147514));
#5344=CARTESIAN_POINT('',(58.5152881956451,-10.2245869045029,4.1231536481525));
#5345=CARTESIAN_POINT('Ctrl Pts',(58.5152881956451,-10.6953934735264,2.67416002147514));
#5346=CARTESIAN_POINT('Ctrl Pts',(58.4654152249681,-10.6373167257333,2.69807208293881));
#5347=CARTESIAN_POINT('Ctrl Pts',(58.4186772780868,-10.5808831001726,2.72773678504619));
#5348=CARTESIAN_POINT('Ctrl Pts',(58.3120945049187,-10.4459731970312,2.81628610756645));
#5349=CARTESIAN_POINT('Ctrl Pts',(58.2507030237862,-10.3615964034925,2.88981038361606));
#5350=CARTESIAN_POINT('Ctrl Pts',(58.1653214105115,-10.21906831722,3.07088795295311));
#5351=CARTESIAN_POINT('Ctrl Pts',(58.1417842183134,-10.1611302121108,3.17882207231172));
#5352=CARTESIAN_POINT('Ctrl Pts',(58.1417842183134,-10.088991757421,3.40084140670788));
#5353=CARTESIAN_POINT('Ctrl Pts',(58.1653214105115,-10.072422585498,3.52221710727082));
#5354=CARTESIAN_POINT('Ctrl Pts',(58.2507030237862,-10.081295504691,3.75248784531307));
#5355=CARTESIAN_POINT('Ctrl Pts',(58.3120945049187,-10.1063412794472,3.86156566901407));
#5356=CARTESIAN_POINT('Ctrl Pts',(58.4186772780868,-10.1634376979201,4.01250162722806));
#5357=CARTESIAN_POINT('Ctrl Pts',(58.4654152249681,-10.1916569856406,4.06967172820396));
#5358=CARTESIAN_POINT('Ctrl Pts',(58.5152881956451,-10.2245869045029,4.12315364815251));
#5359=CARTESIAN_POINT('',(64.5333054217746,-10.6953934735264,2.67416002147514));
#5360=CARTESIAN_POINT('',(65.0333054217745,-10.6953934735264,2.67416002147513));
#5361=CARTESIAN_POINT('',(64.5333054217746,-10.2245869045029,4.1231536481525));
#5362=CARTESIAN_POINT('Ctrl Pts',(64.5333054217746,-10.2245869045029,4.12315364815251));
#5363=CARTESIAN_POINT('Ctrl Pts',(64.5841440169343,-10.1914638560269,4.06935806382539));
#5364=CARTESIAN_POINT('Ctrl Pts',(64.6317941862906,-10.1630893957837,4.01180509073887));
#5365=CARTESIAN_POINT('Ctrl Pts',(64.7397191574786,-10.1061429735371,3.86069838247098));
#5366=CARTESIAN_POINT('Ctrl Pts',(64.8016959801978,-10.0812329983496,3.75191908406943));
#5367=CARTESIAN_POINT('Ctrl Pts',(64.8879780992218,-10.0724580141423,3.5220799008087));
#5368=CARTESIAN_POINT('Ctrl Pts',(64.9118211190309,-10.0889949511726,3.40083157735114));
#5369=CARTESIAN_POINT('Ctrl Pts',(64.9118211190309,-10.1611270183592,3.17883190166846));
#5370=CARTESIAN_POINT('Ctrl Pts',(64.8879780992218,-10.2190163316603,3.0710197797473));
#5371=CARTESIAN_POINT('Ctrl Pts',(64.8016959801978,-10.3612115253291,2.8902337808223));
#5372=CARTESIAN_POINT('Ctrl Pts',(64.7397191574786,-10.4453029859404,2.81687119582945));
#5373=CARTESIAN_POINT('Ctrl Pts',(64.6317941862906,-10.580191903949,2.72809556804404));
#5374=CARTESIAN_POINT('Ctrl Pts',(64.5841440169343,-10.6369761132978,2.69821232401293));
#5375=CARTESIAN_POINT('Ctrl Pts',(64.5333054217746,-10.6953934735264,2.67416002147514));
#5376=CARTESIAN_POINT('',(65.0333054217745,-10.2245869045029,4.12315364815251));
#5377=CARTESIAN_POINT('Origin',(65.0333054217745,-9.83314361665672,6.24030269465341));
#5378=CARTESIAN_POINT('',(58.5152881956451,-9.69434146610128,5.2499825630792));
#5379=CARTESIAN_POINT('',(58.5152881956451,-8.87797608967546,6.53636855793469));
#5380=CARTESIAN_POINT('Ctrl Pts',(58.5152881956451,-9.69434146610128,5.24998256307919));
#5381=CARTESIAN_POINT('Ctrl Pts',(58.4654152249681,-9.63214261826849,5.25870028330521));
#5382=CARTESIAN_POINT('Ctrl Pts',(58.4186772780868,-9.57010464740912,5.27339854227333));
#5383=CARTESIAN_POINT('Ctrl Pts',(58.3120945049187,-9.41741186593077,5.32561519640614));
#5384=CARTESIAN_POINT('Ctrl Pts',(58.2507030237862,-9.31740118060456,5.37584591685751));
#5385=CARTESIAN_POINT('Ctrl Pts',(58.1653214105115,-9.13431871596657,5.51578930768254));
#5386=CARTESIAN_POINT('Ctrl Pts',(58.1417842183134,-9.05135871900561,5.60592385738239));
#5387=CARTESIAN_POINT('Ctrl Pts',(58.1417842183134,-8.9262726633038,5.80302794196643));
#5388=CARTESIAN_POINT('Ctrl Pts',(58.1653214105115,-8.88003913310781,5.91646981620596));
#5389=CARTESIAN_POINT('Ctrl Pts',(58.2507030237862,-8.83136728936705,6.14171278084726));
#5390=CARTESIAN_POINT('Ctrl Pts',(58.3120945049187,-8.82849965338492,6.25359235503467));
#5391=CARTESIAN_POINT('Ctrl Pts',(58.4186772780868,-8.84626603646125,6.41398568443713));
#5392=CARTESIAN_POINT('Ctrl Pts',(58.4654152249681,-8.85938113740538,6.47637753304146));
#5393=CARTESIAN_POINT('Ctrl Pts',(58.5152881956451,-8.87797608967545,6.53636855793469));
#5394=CARTESIAN_POINT('',(64.5333054217746,-9.69434146610128,5.2499825630792));
#5395=CARTESIAN_POINT('',(65.0333054217745,-9.69434146610129,5.24998256307919));
#5396=CARTESIAN_POINT('',(64.5333054217746,-8.87797608967546,6.53636855793469));
#5397=CARTESIAN_POINT('Ctrl Pts',(64.5333054217746,-8.87797608967545,6.53636855793469));
#5398=CARTESIAN_POINT('Ctrl Pts',(64.5841440169343,-8.85927208047261,6.47602569362432));
#5399=CARTESIAN_POINT('Ctrl Pts',(64.6317941862906,-8.84610189845785,6.41322441170358));
#5400=CARTESIAN_POINT('Ctrl Pts',(64.7397191574786,-8.82852326301227,6.25270299921878));
#5401=CARTESIAN_POINT('Ctrl Pts',(64.8016959801978,-8.83144819194687,6.14114634358899));
#5402=CARTESIAN_POINT('Ctrl Pts',(64.8879780992218,-8.88010757055562,5.91634573108268));
#5403=CARTESIAN_POINT('Ctrl Pts',(64.9118211190309,-8.92627820117944,5.80301921567074));
#5404=CARTESIAN_POINT('Ctrl Pts',(64.9118211190309,-9.05135318112997,5.60593258367809));
#5405=CARTESIAN_POINT('Ctrl Pts',(64.8879780992218,-9.13423557963828,5.5159040646126));
#5406=CARTESIAN_POINT('Ctrl Pts',(64.8016959801978,-9.31692309949288,5.37616029695489));
#5407=CARTESIAN_POINT('Ctrl Pts',(64.7397191574786,-9.41661720521969,5.3260152283249));
#5408=CARTESIAN_POINT('Ctrl Pts',(64.6317941862906,-9.5693459406827,5.2735741599327));
#5409=CARTESIAN_POINT('Ctrl Pts',(64.5841440169343,-9.63177783026215,5.25875141157996));
#5410=CARTESIAN_POINT('Ctrl Pts',(64.5333054217746,-9.69434146610128,5.24998256307919));
#5411=CARTESIAN_POINT('',(65.0333054217745,-8.87797608967545,6.5363685579347));
#5412=CARTESIAN_POINT('Origin',(65.0333054217745,-7.97231715504529,8.48965548688909));
#5413=CARTESIAN_POINT('',(58.5152881956451,-8.08415833106712,7.49592939215974));
#5414=CARTESIAN_POINT('',(58.5152881956451,-6.97352938622158,8.53887939213984));
#5415=CARTESIAN_POINT('Ctrl Pts',(58.5152881956451,-8.08415833106713,7.49592939215973));
#5416=CARTESIAN_POINT('Ctrl Pts',(58.4654152249681,-8.02174556555534,7.48890500472477));
#5417=CARTESIAN_POINT('Ctrl Pts',(58.4186772780868,-7.95800132326607,7.48771327488624));
#5418=CARTESIAN_POINT('Ctrl Pts',(58.3120945049187,-7.79711991247583,7.50031629621302));
#5419=CARTESIAN_POINT('Ctrl Pts',(58.2507030237862,-7.68775937453467,7.52409728016453));
#5420=CARTESIAN_POINT('Ctrl Pts',(58.1653214105115,-7.47562627611464,7.6141133345562));
#5421=CARTESIAN_POINT('Ctrl Pts',(58.1417842183134,-7.37285706901645,7.68078482934798));
#5422=CARTESIAN_POINT('Ctrl Pts',(58.1417842183134,-7.20268302921675,7.84058888958737));
#5423=CARTESIAN_POINT('Ctrl Pts',(58.1653214105115,-7.12969016348498,7.93896896733497));
#5424=CARTESIAN_POINT('Ctrl Pts',(58.2507030237862,-7.02653178775528,8.14503131472123));
#5425=CARTESIAN_POINT('Ctrl Pts',(58.3120945049187,-6.99593092515002,8.25268283428457));
#5426=CARTESIAN_POINT('Ctrl Pts',(58.4186772780868,-6.97325094564082,8.41245543210373));
#5427=CARTESIAN_POINT('Ctrl Pts',(58.4654152249681,-6.97043778978239,8.47614871902753));
#5428=CARTESIAN_POINT('Ctrl Pts',(58.5152881956451,-6.97352938622157,8.53887939213984));
#5429=CARTESIAN_POINT('',(64.5333054217746,-8.08415833106712,7.49592939215974));
#5430=CARTESIAN_POINT('',(65.0333054217745,-8.08415833106713,7.49592939215973));
#5431=CARTESIAN_POINT('',(64.5333054217746,-6.97352938622158,8.53887939213984));
#5432=CARTESIAN_POINT('Ctrl Pts',(64.5333054217746,-6.97352938622157,8.53887939213984));
#5433=CARTESIAN_POINT('Ctrl Pts',(64.5841440169343,-6.97041965797865,8.47578081193636));
#5434=CARTESIAN_POINT('Ctrl Pts',(64.6317941862906,-6.97328128516483,8.41167725669145));
#5435=CARTESIAN_POINT('Ctrl Pts',(64.7397191574786,-6.99617496683501,8.25182729069261));
#5436=CARTESIAN_POINT('Ctrl Pts',(64.8016959801978,-7.02675101584963,8.14450279278449));
#5437=CARTESIAN_POINT('Ctrl Pts',(64.8879780992218,-7.12978730955983,7.9388658002752));
#5438=CARTESIAN_POINT('Ctrl Pts',(64.9118211190309,-7.20269056325133,7.84058181465797));
#5439=CARTESIAN_POINT('Ctrl Pts',(64.9118211190309,-7.37284953498187,7.68079190427738));
#5440=CARTESIAN_POINT('Ctrl Pts',(64.8879780992218,-7.47551721277898,7.61420381102219));
#5441=CARTESIAN_POINT('Ctrl Pts',(64.8016959801978,-7.68721813006929,7.52428288949532));
#5442=CARTESIAN_POINT('Ctrl Pts',(64.7397191574786,-7.79625073359953,7.50050613631087));
#5443=CARTESIAN_POINT('Ctrl Pts',(64.6317941862906,-7.95722277837073,7.48769469250372));
#5444=CARTESIAN_POINT('Ctrl Pts',(64.5841440169343,-8.02137952295014,7.48886380762261));
#5445=CARTESIAN_POINT('Ctrl Pts',(64.5333054217746,-8.08415833106713,7.49592939215973));
#5446=CARTESIAN_POINT('',(65.0333054217745,-6.97352938622157,8.53887939213985));
#5447=CARTESIAN_POINT('Origin',(65.0333054217745,-5.61056068645084,10.2055720021147));
#5448=CARTESIAN_POINT('',(58.5152881956451,-5.96601779663743,9.270879409431));
#5449=CARTESIAN_POINT('',(58.5152881956451,-4.63091018458434,10.0048610303352));
#5450=CARTESIAN_POINT('Ctrl Pts',(58.5152881956451,-5.96601779663743,9.270879409431));
#5451=CARTESIAN_POINT('Ctrl Pts',(58.4654152249681,-5.90731273704185,9.24855428243148));
#5452=CARTESIAN_POINT('Ctrl Pts',(58.4186772780868,-5.84586750850063,9.23154744455494));
#5453=CARTESIAN_POINT('Ctrl Pts',(58.3120945049187,-5.6869062391189,9.20374493889505));
#5454=CARTESIAN_POINT('Ctrl Pts',(58.2507030237862,-5.57506737336155,9.19958193966467));
#5455=CARTESIAN_POINT('Ctrl Pts',(58.1653214105115,-5.34721274390418,9.23401461786969));
#5456=CARTESIAN_POINT('Ctrl Pts',(58.1417842183134,-5.23109169390945,9.273033842535));
#5457=CARTESIAN_POINT('Ctrl Pts',(58.1417842183134,-5.0265223307888,9.38549680160669));
#5458=CARTESIAN_POINT('Ctrl Pts',(58.1653214105115,-4.93135653972418,9.46263350076087));
#5459=CARTESIAN_POINT('Ctrl Pts',(58.2507030237862,-4.78019345214259,9.63656757576151));
#5460=CARTESIAN_POINT('Ctrl Pts',(58.3120945049187,-4.72378212765379,9.73322689981202));
#5461=CARTESIAN_POINT('Ctrl Pts',(58.4186772780868,-4.66208085208275,9.88233966612439));
#5462=CARTESIAN_POINT('Ctrl Pts',(58.4654152249681,-4.64351620035041,9.9433323079027));
#5463=CARTESIAN_POINT('Ctrl Pts',(58.5152881956451,-4.63091018458433,10.0048610303352));
#5464=CARTESIAN_POINT('',(64.5333054217746,-5.96601779663743,9.270879409431));
#5465=CARTESIAN_POINT('',(65.0333054217745,-5.96601779663744,9.270879409431));
#5466=CARTESIAN_POINT('',(64.5333054217746,-4.63091018458434,10.0048610303352));
#5467=CARTESIAN_POINT('Ctrl Pts',(64.5333054217746,-4.63091018458433,10.0048610303352));
#5468=CARTESIAN_POINT('Ctrl Pts',(64.5841440169343,-4.64359013296362,9.94297145009311));
#5469=CARTESIAN_POINT('Ctrl Pts',(64.6317941862906,-4.66230376279031,9.88159348365645));
#5470=CARTESIAN_POINT('Ctrl Pts',(64.7397191574786,-4.72423126735984,9.73245892539434));
#5471=CARTESIAN_POINT('Ctrl Pts',(64.8016959801978,-4.78053723084403,9.63611017812334));
#5472=CARTESIAN_POINT('Ctrl Pts',(64.8879780992218,-4.9314762903809,9.46255773413038));
#5473=CARTESIAN_POINT('Ctrl Pts',(64.9118211190309,-5.02653138759124,9.38549182258742));
#5474=CARTESIAN_POINT('Ctrl Pts',(64.9118211190309,-5.23108263710702,9.27303882155427));
#5475=CARTESIAN_POINT('Ctrl Pts',(64.8879780992218,-5.34708460641165,9.23407512890247));
#5476=CARTESIAN_POINT('Ctrl Pts',(64.8016959801978,-5.5744969739228,9.19962711571201));
#5477=CARTESIAN_POINT('Ctrl Pts',(64.7397191574786,-5.68601715578279,9.20371265882047));
#5478=CARTESIAN_POINT('Ctrl Pts',(64.6317941862906,-5.84511804427543,9.23133582972995));
#5479=CARTESIAN_POINT('Ctrl Pts',(64.5841440169343,-5.90696843964088,9.24842334851785));
#5480=CARTESIAN_POINT('Ctrl Pts',(64.5333054217746,-5.96601779663743,9.270879409431));
#5481=CARTESIAN_POINT('',(65.0333054217745,-4.63091018458433,10.0048610303352));
#5482=CARTESIAN_POINT('Origin',(65.0333054217745,-2.89627205572787,11.2802348949791));
#5483=CARTESIAN_POINT('',(58.5152881956451,-3.47301042256638,10.4633059774983));
#5484=CARTESIAN_POINT('',(58.5152881956451,-1.99731386475336,10.8422004546895));
#5485=CARTESIAN_POINT('Ctrl Pts',(58.5152881956451,-3.47301042256638,10.4633059774983));
#5486=CARTESIAN_POINT('Ctrl Pts',(58.4654152249681,-3.4217017236835,10.4270828807697));
#5487=CARTESIAN_POINT('Ctrl Pts',(58.4186772780868,-3.36641633857933,10.3953295370257));
#5488=CARTESIAN_POINT('Ctrl Pts',(58.3120945049187,-3.21936333178,10.3288684380602));
#5489=CARTESIAN_POINT('Ctrl Pts',(58.2507030237862,-3.11207338545658,10.2970230322));
#5490=CARTESIAN_POINT('Ctrl Pts',(58.1653214105115,-2.88281416932138,10.2737088024122));
#5491=CARTESIAN_POINT('Ctrl Pts',(58.1417842183134,-2.76063758906464,10.2826240355627));
#5492=CARTESIAN_POINT('Ctrl Pts',(58.1417842183134,-2.5345267480614,10.3406794321384));
#5493=CARTESIAN_POINT('Ctrl Pts',(58.1653214105115,-2.4231676483118,10.3917259702023));
#5494=CARTESIAN_POINT('Ctrl Pts',(58.2507030237862,-2.23349798161003,10.5226028552003));
#5495=CARTESIAN_POINT('Ctrl Pts',(58.3120945049187,-2.15482072622166,10.6021965229197));
#5496=CARTESIAN_POINT('Ctrl Pts',(58.4186772780868,-2.05797507265433,10.7312801542195));
#5497=CARTESIAN_POINT('Ctrl Pts',(58.4654152249681,-2.02482541039243,10.7857397588542));
#5498=CARTESIAN_POINT('Ctrl Pts',(58.5152881956451,-1.99731386475336,10.8422004546895));
#5499=CARTESIAN_POINT('',(64.5333054217746,-3.47301042256638,10.4633059774983));
#5500=CARTESIAN_POINT('',(65.0333054217745,-3.47301042256639,10.4633059774983));
#5501=CARTESIAN_POINT('',(64.5333054217746,-1.99731386475336,10.8422004546895));
#5502=CARTESIAN_POINT('Ctrl Pts',(64.5333054217746,-1.99731386475336,10.8422004546895));
#5503=CARTESIAN_POINT('Ctrl Pts',(64.5841440169343,-2.0249867619646,10.7854086243495));
#5504=CARTESIAN_POINT('Ctrl Pts',(64.6317941862906,-2.05837654824586,10.7306128500846));
#5505=CARTESIAN_POINT('Ctrl Pts',(64.7397191574786,-2.15544674284921,10.6015643723334));
#5506=CARTESIAN_POINT('Ctrl Pts',(64.8016959801978,-2.23394471003843,10.5222453218365));
#5507=CARTESIAN_POINT('Ctrl Pts',(64.8879780992218,-2.42330247917622,10.3916823646972));
#5508=CARTESIAN_POINT('Ctrl Pts',(64.9118211190309,-2.53453675855947,10.3406768618793));
#5509=CARTESIAN_POINT('Ctrl Pts',(64.9118211190309,-2.76062757856657,10.2826266058217));
#5510=CARTESIAN_POINT('Ctrl Pts',(64.8879780992218,-2.88267500902189,10.2737355458811));
#5511=CARTESIAN_POINT('Ctrl Pts',(64.8016959801978,-3.11150967133898,10.2969249363867));
#5512=CARTESIAN_POINT('Ctrl Pts',(64.7397191574786,-3.21851020835992,10.328616066089));
#5513=CARTESIAN_POINT('Ctrl Pts',(64.6317941862906,-3.36574304661788,10.3949381862959));
#5514=CARTESIAN_POINT('Ctrl Pts',(64.5841440169343,-3.42140080495871,10.4268704371039));
#5515=CARTESIAN_POINT('Ctrl Pts',(64.5333054217746,-3.47301042256638,10.4633059774983));
#5516=CARTESIAN_POINT('',(65.0333054217745,-1.99731386475336,10.8422004546896));
#5517=CARTESIAN_POINT('Origin',(64.7833054217745,0.,0.));
#5518=CARTESIAN_POINT('',(65.0333054217745,-1.28889603700374E-15,10.5246348408465));
#5519=CARTESIAN_POINT('Origin',(65.0333054217745,0.,0.));
#5520=CARTESIAN_POINT('',(64.911821119031,-7.73317429945324E-16,10.6461191435901));
#5521=CARTESIAN_POINT('',(64.7833054217745,-1.31951220698242E-15,10.7746348408465));
#5522=CARTESIAN_POINT('',(64.5333054217746,-0.761781030806626,10.9982845496518));
#5523=CARTESIAN_POINT('Ctrl Pts',(64.911821119031,-2.60208521396521E-16,
10.6461191435901));
#5524=CARTESIAN_POINT('Ctrl Pts',(64.911821119031,-0.116712136386744,10.6461191435901));
#5525=CARTESIAN_POINT('Ctrl Pts',(64.8879780992218,-0.237136339078202,10.6678593743557));
#5526=CARTESIAN_POINT('Ctrl Pts',(64.8016959801978,-0.453014772772831,10.7472290938673));
#5527=CARTESIAN_POINT('Ctrl Pts',(64.7397191574786,-0.548772427693239,10.8045345399324));
#5528=CARTESIAN_POINT('Ctrl Pts',(64.6317941862906,-0.674886035004275,10.9053883467085));
#5529=CARTESIAN_POINT('Ctrl Pts',(64.5841440169343,-0.720853974669018,10.9501589087797));
#5530=CARTESIAN_POINT('Ctrl Pts',(64.5333054217746,-0.761781030806632,10.9982845496518));
#5531=CARTESIAN_POINT('Origin',(64.5333054217746,0.,0.));
#5532=CARTESIAN_POINT('Origin',(64.5333054217746,0.,0.));
#5533=CARTESIAN_POINT('Origin',(64.5333054217746,0.,0.));
#5534=CARTESIAN_POINT('Origin',(64.5333054217746,0.,0.));
#5535=CARTESIAN_POINT('Origin',(64.5333054217746,0.,0.));
#5536=CARTESIAN_POINT('Origin',(64.5333054217746,0.,0.));
#5537=CARTESIAN_POINT('Origin',(64.5333054217746,0.,0.));
#5538=CARTESIAN_POINT('Origin',(64.5333054217746,0.,0.));
#5539=CARTESIAN_POINT('Origin',(64.5333054217746,0.,0.));
#5540=CARTESIAN_POINT('Origin',(64.5333054217746,0.,0.));
#5541=CARTESIAN_POINT('Origin',(64.5333054217746,0.,0.));
#5542=CARTESIAN_POINT('Origin',(64.5333054217746,0.,0.));
#5543=CARTESIAN_POINT('Origin',(64.5333054217746,0.,0.));
#5544=CARTESIAN_POINT('Origin',(64.5333054217746,0.,0.));
#5545=CARTESIAN_POINT('Origin',(64.5333054217746,0.,0.));
#5546=CARTESIAN_POINT('Origin',(64.5333054217746,0.,0.));
#5547=CARTESIAN_POINT('Origin',(64.5333054217746,0.,0.));
#5548=CARTESIAN_POINT('Origin',(64.5333054217746,0.,0.));
#5549=CARTESIAN_POINT('Origin',(64.5333054217746,0.,0.));
#5550=CARTESIAN_POINT('Origin',(64.5333054217746,0.,0.));
#5551=CARTESIAN_POINT('Origin',(64.5333054217746,0.,0.));
#5552=CARTESIAN_POINT('Origin',(64.5333054217746,0.,0.));
#5553=CARTESIAN_POINT('Origin',(64.5333054217746,0.,0.));
#5554=CARTESIAN_POINT('Origin',(64.5333054217746,0.,0.));
#5555=CARTESIAN_POINT('',(64.5333054217746,0.761781030806626,10.9982845496518));
#5556=CARTESIAN_POINT('Origin',(64.5333054217746,0.,0.));
#5557=CARTESIAN_POINT('Ctrl Pts',(64.5333054217746,0.761781030806632,10.9982845496518));
#5558=CARTESIAN_POINT('Ctrl Pts',(64.5841440169343,0.720853974669017,10.9501589087797));
#5559=CARTESIAN_POINT('Ctrl Pts',(64.6317941862906,0.674886035004276,10.9053883467085));
#5560=CARTESIAN_POINT('Ctrl Pts',(64.7397191574786,0.548772427693241,10.8045345399324));
#5561=CARTESIAN_POINT('Ctrl Pts',(64.8016959801978,0.453014772772831,10.7472290938673));
#5562=CARTESIAN_POINT('Ctrl Pts',(64.8879780992218,0.237136339078202,10.6678593743557));
#5563=CARTESIAN_POINT('Ctrl Pts',(64.911821119031,0.116712136386744,10.6461191435901));
#5564=CARTESIAN_POINT('Ctrl Pts',(64.911821119031,7.97972798949331E-16,
10.6461191435901));
#5565=CARTESIAN_POINT('Origin',(61.5242968087098,0.,0.));
#5566=CARTESIAN_POINT('',(58.5152881956451,0.761781030806626,10.9982845496518));
#5567=CARTESIAN_POINT('Origin',(58.5152881956451,0.,0.));
#5568=CARTESIAN_POINT('',(65.0333054217745,0.761781030806634,10.9982845496518));
#5569=CARTESIAN_POINT('Origin',(61.5242968087098,0.,0.));
#5570=CARTESIAN_POINT('',(58.5152881956451,-0.761781030806626,10.9982845496518));
#5571=CARTESIAN_POINT('',(65.0333054217745,-0.761781030806634,10.9982845496518));
#5572=CARTESIAN_POINT('Origin',(58.5152881956451,0.,0.));
#5573=CARTESIAN_POINT('Origin',(61.5242968087098,0.,0.));
#5574=CARTESIAN_POINT('Origin',(58.5152881956451,0.,0.));
#5575=CARTESIAN_POINT('Origin',(61.5242968087098,0.,0.));
#5576=CARTESIAN_POINT('Origin',(58.5152881956451,0.,0.));
#5577=CARTESIAN_POINT('Origin',(61.5242968087098,0.,0.));
#5578=CARTESIAN_POINT('Origin',(58.5152881956451,0.,0.));
#5579=CARTESIAN_POINT('Origin',(61.5242968087098,0.,0.));
#5580=CARTESIAN_POINT('Origin',(58.5152881956451,0.,0.));
#5581=CARTESIAN_POINT('Origin',(61.5242968087098,0.,0.));
#5582=CARTESIAN_POINT('Origin',(58.5152881956451,0.,0.));
#5583=CARTESIAN_POINT('Origin',(61.5242968087098,0.,0.));
#5584=CARTESIAN_POINT('Origin',(58.5152881956451,0.,0.));
#5585=CARTESIAN_POINT('Origin',(61.5242968087098,0.,0.));
#5586=CARTESIAN_POINT('Origin',(58.5152881956451,0.,0.));
#5587=CARTESIAN_POINT('Origin',(61.5242968087098,0.,0.));
#5588=CARTESIAN_POINT('Origin',(58.5152881956451,0.,0.));
#5589=CARTESIAN_POINT('Origin',(61.5242968087098,0.,0.));
#5590=CARTESIAN_POINT('Origin',(58.5152881956451,0.,0.));
#5591=CARTESIAN_POINT('Origin',(61.5242968087098,0.,0.));
#5592=CARTESIAN_POINT('Origin',(58.5152881956451,0.,0.));
#5593=CARTESIAN_POINT('Origin',(61.5242968087098,0.,0.));
#5594=CARTESIAN_POINT('Origin',(58.5152881956451,0.,0.));
#5595=CARTESIAN_POINT('Origin',(61.5242968087098,0.,0.));
#5596=CARTESIAN_POINT('Origin',(58.5152881956451,0.,0.));
#5597=CARTESIAN_POINT('Origin',(61.5242968087098,0.,0.));
#5598=CARTESIAN_POINT('Origin',(58.5152881956451,0.,0.));
#5599=CARTESIAN_POINT('Origin',(61.5242968087098,0.,0.));
#5600=CARTESIAN_POINT('Origin',(58.5152881956451,0.,0.));
#5601=CARTESIAN_POINT('Origin',(61.5242968087098,0.,0.));
#5602=CARTESIAN_POINT('Origin',(58.5152881956451,0.,0.));
#5603=CARTESIAN_POINT('Origin',(61.5242968087098,0.,0.));
#5604=CARTESIAN_POINT('Origin',(58.5152881956451,0.,0.));
#5605=CARTESIAN_POINT('Origin',(61.5242968087098,0.,0.));
#5606=CARTESIAN_POINT('Origin',(58.5152881956451,0.,0.));
#5607=CARTESIAN_POINT('Origin',(61.5242968087098,0.,0.));
#5608=CARTESIAN_POINT('Origin',(58.5152881956451,0.,0.));
#5609=CARTESIAN_POINT('Origin',(61.5242968087098,0.,0.));
#5610=CARTESIAN_POINT('Origin',(58.5152881956451,0.,0.));
#5611=CARTESIAN_POINT('Origin',(61.5242968087098,0.,0.));
#5612=CARTESIAN_POINT('Origin',(58.5152881956451,0.,0.));
#5613=CARTESIAN_POINT('Origin',(61.5242968087098,0.,0.));
#5614=CARTESIAN_POINT('Origin',(58.5152881956451,0.,0.));
#5615=CARTESIAN_POINT('Origin',(61.5242968087098,0.,0.));
#5616=CARTESIAN_POINT('Origin',(58.5152881956451,0.,0.));
#5617=CARTESIAN_POINT('Origin',(65.0333054217745,0.,11.6461191435901));
#5618=CARTESIAN_POINT('',(58.1417842183134,-5.99845082347644E-16,10.6461191435901));
#5619=CARTESIAN_POINT('Ctrl Pts',(58.5152881956451,-0.761781030806632,10.9982845496518));
#5620=CARTESIAN_POINT('Ctrl Pts',(58.4654152249681,-0.721092606887457,10.9504395135808));
#5621=CARTESIAN_POINT('Ctrl Pts',(58.4186772780868,-0.675440849291838,10.9059348433374));
#5622=CARTESIAN_POINT('Ctrl Pts',(58.3120945049187,-0.549535986315256,10.8049911463411));
#5623=CARTESIAN_POINT('Ctrl Pts',(58.2507030237862,-0.453536381338077,10.7474642978206));
#5624=CARTESIAN_POINT('Ctrl Pts',(58.1653214105115,-0.237277778231237,10.6678680788412));
#5625=CARTESIAN_POINT('Ctrl Pts',(58.1417842183134,-0.11672247158404,10.6461191435901));
#5626=CARTESIAN_POINT('Ctrl Pts',(58.1417842183134,-6.93889390390723E-17,
10.6461191435901));
#5627=CARTESIAN_POINT('Ctrl Pts',(58.1417842183134,1.38777878078145E-16,
10.6461191435901));
#5628=CARTESIAN_POINT('Ctrl Pts',(58.1417842183134,0.11672247158404,10.6461191435901));
#5629=CARTESIAN_POINT('Ctrl Pts',(58.1653214105115,0.237277778231238,10.6678680788412));
#5630=CARTESIAN_POINT('Ctrl Pts',(58.2507030237862,0.453536381338078,10.7474642978206));
#5631=CARTESIAN_POINT('Ctrl Pts',(58.3120945049187,0.549535986315257,10.8049911463411));
#5632=CARTESIAN_POINT('Ctrl Pts',(58.4186772780868,0.675440849291838,10.9059348433374));
#5633=CARTESIAN_POINT('Ctrl Pts',(58.4654152249681,0.721092606887457,10.9504395135808));
#5634=CARTESIAN_POINT('Ctrl Pts',(58.5152881956451,0.761781030806632,10.9982845496518));
#5635=CARTESIAN_POINT('Origin',(58.259303580337,0.,0.));
#5636=CARTESIAN_POINT('Origin',(58.5152881956451,0.,0.));
#5637=CARTESIAN_POINT('',(58.259303580337,-1.31835865745385E-15,10.765215394118));
#5638=CARTESIAN_POINT('Origin',(61.5242968087098,0.,0.));
#5639=CARTESIAN_POINT('Origin',(65.0333054217745,0.,0.));
#5640=CARTESIAN_POINT('Origin',(57.9998593353039,0.,-9.50579594738959));
#5641=CARTESIAN_POINT('',(57.9998593353039,-1.16412425803185E-15,9.50579594738959));
#5642=CARTESIAN_POINT('Origin',(57.9998593353039,0.,0.));
#5643=CARTESIAN_POINT('Origin',(54.0059764245311,0.,0.));
#5644=CARTESIAN_POINT('',(54.0059764245311,-1.16412425803185E-15,9.50579594738959));
#7293=UNCERTAINTY_MEASURE_WITH_UNIT(LENGTH_MEASURE(0.01),#7316,
'DISTANCE_ACCURACY_VALUE',
'Maximum model space distance between geometric entities at asserted c
onnectivities');
#7303=UNCERTAINTY_MEASURE_WITH_UNIT(LENGTH_MEASURE(0.01),#7316,
'DISTANCE_ACCURACY_VALUE',
'Maximum model space distance between geometric entities at asserted c
onnectivities');
#7305=(
GEOMETRIC_REPRESENTATION_CONTEXT(3)
GLOBAL_UNCERTAINTY_ASSIGNED_CONTEXT((#7293))
GLOBAL_UNIT_ASSIGNED_CONTEXT((#7316,#7318,#7319))
REPRESENTATION_CONTEXT('','3D')
);
#7315=(
GEOMETRIC_REPRESENTATION_CONTEXT(3)
GLOBAL_UNCERTAINTY_ASSIGNED_CONTEXT((#7303))
GLOBAL_UNIT_ASSIGNED_CONTEXT((#7316,#7318,#7319))
REPRESENTATION_CONTEXT('','3D')
);
#7316=(
LENGTH_UNIT()
NAMED_UNIT(*)
SI_UNIT(.MILLI.,.METRE.)
);
#7318=(
NAMED_UNIT(*)
PLANE_ANGLE_UNIT()
SI_UNIT($,.RADIAN.)
);
#7319=(
NAMED_UNIT(*)
SI_UNIT($,.STERADIAN.)
SOLID_ANGLE_UNIT()
);
#7321=SHAPE_DEFINITION_REPRESENTATION(#7332,#7353);
#7332=PRODUCT_DEFINITION_SHAPE('',$,#7365);
#7353=SHAPE_REPRESENTATION('',(#3336),#7305);
#7363=PRODUCT_DEFINITION_CONTEXT('part definition',#7398,'design');
#7365=PRODUCT_DEFINITION('End_Cap','End_Cap',#7376,#7363);
#7376=PRODUCT_DEFINITION_FORMATION('',$,#7401);
#7398=APPLICATION_CONTEXT(
'Core Data for Automotive Mechanical Design Process');
#7399=PRODUCT_CONTEXT('part definition',#7398,'mechanical');
#7401=PRODUCT('End_Cap','End_Cap',$,(#7399));
#7453=COLOUR_RGB('Off White',0.89,0.88,0.83);
#7454=FILL_AREA_STYLE_COLOUR('',#7453);
#7455=FILL_AREA_STYLE('',(#7454));
#7456=SURFACE_STYLE_FILL_AREA(#7455);
#7457=SURFACE_SIDE_STYLE('',(#7456));
#7458=SURFACE_STYLE_USAGE(.BOTH.,#7457);
#7459=PRESENTATION_STYLE_ASSIGNMENT((#7458));
ENDSEC;
END-ISO-10303-21;
